ISO-10303-21;
HEADER;
/* Generated by software containing ST-Developer
 * from STEP Tools, Inc. (www.steptools.com) 
 */

FILE_DESCRIPTION(
/* description */ (''),
/* implementation_level */ '2;1');

FILE_NAME(
/* name */ '15_Drain_Plug_M18x1.5.step',
/* time_stamp */ '2026-10-26T07:49:00-07:00',
/* author */ (''),
/* organization */ (''),
/* preprocessor_version */ 'ST-DEVELOPER v20.2',
/* originating_system */ 'Autodesk Translation Framework v15.15.0.0',
/* authorisation */ '');

FILE_SCHEMA (('AUTOMOTIVE_DESIGN { 1 0 10303 214 3 1 1 }'));
ENDSEC;

DATA;
#10=MECHANICAL_DESIGN_GEOMETRIC_PRESENTATION_REPRESENTATION('',(#191),#38507);
#161=SHAPE_REPRESENTATION_RELATIONSHIP('SRR','None',#38589,#176);
#176=ADVANCED_BREP_SHAPE_REPRESENTATION('',(#206),#38506);
#191=STYLED_ITEM('',(#38706),#206);
#206=MANIFOLD_SOLID_BREP('Body1',#15085);
#254=B_SPLINE_SURFACE_WITH_KNOTS('',3,3,((#37108,#37109,#37110,#37111,#37112,
#37113,#37114,#37115,#37116,#37117,#37118,#37119,#37120,#37121,#37122,#37123,
#37124,#37125,#37126,#37127,#37128,#37129,#37130,#37131,#37132,#37133,#37134,
#37135,#37136,#37137,#37138,#37139,#37140,#37141,#37142,#37143,#37144,#37145,
#37146,#37147,#37148,#37149,#37150,#37151,#37152,#37153,#37154,#37155,#37156,
#37157,#37158,#37159,#37160,#37161,#37162,#37163,#37164,#37165,#37166,#37167,
#37168,#37169,#37170,#37171,#37172,#37173,#37174,#37175,#37176,#37177,#37178,
#37179,#37180,#37181,#37182,#37183,#37184,#37185,#37186,#37187,#37188,#37189,
#37190,#37191,#37192,#37193,#37194,#37195,#37196,#37197,#37198,#37199,#37200),
(#37201,#37202,#37203,#37204,#37205,#37206,#37207,#37208,#37209,#37210,
#37211,#37212,#37213,#37214,#37215,#37216,#37217,#37218,#37219,#37220,#37221,
#37222,#37223,#37224,#37225,#37226,#37227,#37228,#37229,#37230,#37231,#37232,
#37233,#37234,#37235,#37236,#37237,#37238,#37239,#37240,#37241,#37242,#37243,
#37244,#37245,#37246,#37247,#37248,#37249,#37250,#37251,#37252,#37253,#37254,
#37255,#37256,#37257,#37258,#37259,#37260,#37261,#37262,#37263,#37264,#37265,
#37266,#37267,#37268,#37269,#37270,#37271,#37272,#37273,#37274,#37275,#37276,
#37277,#37278,#37279,#37280,#37281,#37282,#37283,#37284,#37285,#37286,#37287,
#37288,#37289,#37290,#37291,#37292,#37293),(#37294,#37295,#37296,#37297,
#37298,#37299,#37300,#37301,#37302,#37303,#37304,#37305,#37306,#37307,#37308,
#37309,#37310,#37311,#37312,#37313,#37314,#37315,#37316,#37317,#37318,#37319,
#37320,#37321,#37322,#37323,#37324,#37325,#37326,#37327,#37328,#37329,#37330,
#37331,#37332,#37333,#37334,#37335,#37336,#37337,#37338,#37339,#37340,#37341,
#37342,#37343,#37344,#37345,#37346,#37347,#37348,#37349,#37350,#37351,#37352,
#37353,#37354,#37355,#37356,#37357,#37358,#37359,#37360,#37361,#37362,#37363,
#37364,#37365,#37366,#37367,#37368,#37369,#37370,#37371,#37372,#37373,#37374,
#37375,#37376,#37377,#37378,#37379,#37380,#37381,#37382,#37383,#37384,#37385,
#37386),(#37387,#37388,#37389,#37390,#37391,#37392,#37393,#37394,#37395,
#37396,#37397,#37398,#37399,#37400,#37401,#37402,#37403,#37404,#37405,#37406,
#37407,#37408,#37409,#37410,#37411,#37412,#37413,#37414,#37415,#37416,#37417,
#37418,#37419,#37420,#37421,#37422,#37423,#37424,#37425,#37426,#37427,#37428,
#37429,#37430,#37431,#37432,#37433,#37434,#37435,#37436,#37437,#37438,#37439,
#37440,#37441,#37442,#37443,#37444,#37445,#37446,#37447,#37448,#37449,#37450,
#37451,#37452,#37453,#37454,#37455,#37456,#37457,#37458,#37459,#37460,#37461,
#37462,#37463,#37464,#37465,#37466,#37467,#37468,#37469,#37470,#37471,#37472,
#37473,#37474,#37475,#37476,#37477,#37478,#37479)),.UNSPECIFIED.,.F.,.F.,
 .F.,(4,4),(4,1,1,1,1,1,1,1,1,1,1,1,1,1,1,1,1,1,1,1,1,1,1,1,1,1,1,1,1,1,
1,1,1,1,1,1,1,1,1,1,1,1,1,1,1,1,1,1,1,1,1,1,1,1,1,1,1,1,1,1,1,1,1,1,1,1,
1,1,1,1,1,1,1,1,1,1,1,1,1,1,1,1,1,1,1,1,1,1,1,1,4),(0.,0.0989001011121829),
(8.30505915324879,8.79698604421743,9.28891293518608,9.78083982615473,10.2727667171234,
10.764693608092,11.2566204990607,11.7485473900293,12.240474280998,12.7324011719666,
13.2243280629353,13.7162549539039,14.2081818448726,14.7001087358412,15.1920356268099,
15.6839625177785,16.1758894087472,16.6678162997158,17.1597431906845,17.6516700816531,
18.1435969726218,18.6355238635904,19.127450754559,19.6193776455277,20.1113045364963,
20.603231427465,21.0951583184336,21.5870852094023,22.0790121003709,22.5709389913396,
23.0628658823082,23.5547927732769,24.0467196642455,24.5386465552142,25.0305734461828,
25.5225003371515,26.0144272281201,26.5063541190888,26.9982810100574,27.4902079010261,
27.9821347919947,28.4740616829634,28.965988573932,29.4579154649007,29.9498423558693,
30.441769246838,30.9336961378066,31.4256230287753,31.9175499197439,32.4094768107125,
32.9014037016812,33.3933305926498,33.8852574836185,34.3771843745871,34.8691112655558,
35.3610381565244,35.8529650474931,36.3448919384617,36.8368188294304,37.328745720399,
37.8206726113677,38.3125995023363,38.804526393305,39.2964532842736,39.7883801752423,
40.2803070662109,40.7722339571796,41.2641608481482,41.7560877391169,42.2480146300855,
42.7399415210542,43.2318684120228,43.7237953029915,44.2157221939601,44.7076490849288,
45.1995759758974,45.6915028668661,46.1834297578347,46.6753566488034,47.167283539772,
47.6592104307407,48.1511373217093,48.6430642126779,49.1349911036466,49.6269179946152,
50.1188448855839,50.6107717765525,51.1026986675212,51.5946255584898,52.0865524494585,
52.5784793404271),.UNSPECIFIED.);
#255=B_SPLINE_SURFACE_WITH_KNOTS('',3,3,((#37895,#37896,#37897,#37898,#37899,
#37900,#37901,#37902,#37903,#37904,#37905,#37906,#37907,#37908,#37909,#37910,
#37911,#37912,#37913,#37914,#37915,#37916,#37917,#37918,#37919,#37920,#37921,
#37922,#37923,#37924,#37925,#37926,#37927,#37928,#37929,#37930,#37931,#37932,
#37933,#37934,#37935,#37936,#37937,#37938,#37939,#37940,#37941,#37942,#37943,
#37944,#37945,#37946,#37947,#37948,#37949,#37950,#37951,#37952,#37953,#37954,
#37955,#37956,#37957,#37958,#37959,#37960,#37961,#37962,#37963,#37964,#37965,
#37966,#37967,#37968,#37969,#37970,#37971,#37972,#37973,#37974,#37975,#37976,
#37977,#37978,#37979,#37980,#37981,#37982,#37983,#37984,#37985,#37986,#37987),
(#37988,#37989,#37990,#37991,#37992,#37993,#37994,#37995,#37996,#37997,
#37998,#37999,#38000,#38001,#38002,#38003,#38004,#38005,#38006,#38007,#38008,
#38009,#38010,#38011,#38012,#38013,#38014,#38015,#38016,#38017,#38018,#38019,
#38020,#38021,#38022,#38023,#38024,#38025,#38026,#38027,#38028,#38029,#38030,
#38031,#38032,#38033,#38034,#38035,#38036,#38037,#38038,#38039,#38040,#38041,
#38042,#38043,#38044,#38045,#38046,#38047,#38048,#38049,#38050,#38051,#38052,
#38053,#38054,#38055,#38056,#38057,#38058,#38059,#38060,#38061,#38062,#38063,
#38064,#38065,#38066,#38067,#38068,#38069,#38070,#38071,#38072,#38073,#38074,
#38075,#38076,#38077,#38078,#38079,#38080),(#38081,#38082,#38083,#38084,
#38085,#38086,#38087,#38088,#38089,#38090,#38091,#38092,#38093,#38094,#38095,
#38096,#38097,#38098,#38099,#38100,#38101,#38102,#38103,#38104,#38105,#38106,
#38107,#38108,#38109,#38110,#38111,#38112,#38113,#38114,#38115,#38116,#38117,
#38118,#38119,#38120,#38121,#38122,#38123,#38124,#38125,#38126,#38127,#38128,
#38129,#38130,#38131,#38132,#38133,#38134,#38135,#38136,#38137,#38138,#38139,
#38140,#38141,#38142,#38143,#38144,#38145,#38146,#38147,#38148,#38149,#38150,
#38151,#38152,#38153,#38154,#38155,#38156,#38157,#38158,#38159,#38160,#38161,
#38162,#38163,#38164,#38165,#38166,#38167,#38168,#38169,#38170,#38171,#38172,
#38173),(#38174,#38175,#38176,#38177,#38178,#38179,#38180,#38181,#38182,
#38183,#38184,#38185,#38186,#38187,#38188,#38189,#38190,#38191,#38192,#38193,
#38194,#38195,#38196,#38197,#38198,#38199,#38200,#38201,#38202,#38203,#38204,
#38205,#38206,#38207,#38208,#38209,#38210,#38211,#38212,#38213,#38214,#38215,
#38216,#38217,#38218,#38219,#38220,#38221,#38222,#38223,#38224,#38225,#38226,
#38227,#38228,#38229,#38230,#38231,#38232,#38233,#38234,#38235,#38236,#38237,
#38238,#38239,#38240,#38241,#38242,#38243,#38244,#38245,#38246,#38247,#38248,
#38249,#38250,#38251,#38252,#38253,#38254,#38255,#38256,#38257,#38258,#38259,
#38260,#38261,#38262,#38263,#38264,#38265,#38266)),.UNSPECIFIED.,.F.,.F.,
 .F.,(4,4),(4,1,1,1,1,1,1,1,1,1,1,1,1,1,1,1,1,1,1,1,1,1,1,1,1,1,1,1,1,1,
1,1,1,1,1,1,1,1,1,1,1,1,1,1,1,1,1,1,1,1,1,1,1,1,1,1,1,1,1,1,1,1,1,1,1,1,
1,1,1,1,1,1,1,1,1,1,1,1,1,1,1,1,1,1,1,1,1,1,1,1,4),(0.,0.0989001011121829),
(11.6147305479243,12.1066574388929,12.5985843298616,13.0905112208302,13.5824381117989,
14.0743650027675,14.5662918937362,15.0582187847048,15.5501456756735,16.0420725666421,
16.5339994576108,17.0259263485794,17.5178532395481,18.0097801305167,18.5017070214854,
18.993633912454,19.4855608034226,19.9774876943913,20.4694145853599,20.9613414763286,
21.4532683672972,21.9451952582659,22.4371221492345,22.9290490402032,23.4209759311718,
23.9129028221405,24.4048297131091,24.8967566040778,25.3886834950464,25.8806103860151,
26.3725372769837,26.8644641679524,27.356391058921,27.8483179498897,28.3402448408583,
28.832171731827,29.3240986227956,29.8160255137643,30.3079524047329,30.7998792957016,
31.2918061866702,31.7837330776389,32.2756599686075,32.7675868595761,33.2595137505448,
33.7514406415134,34.2433675324821,34.7352944234507,35.2272213144194,35.719148205388,
36.2110750963567,36.7030019873253,37.194928878294,37.6868557692626,38.1787826602313,
38.6707095511999,39.1626364421686,39.6545633331372,40.1464902241059,40.6384171150745,
41.1303440060432,41.6222708970118,42.1141977879805,42.6061246789491,43.0980515699178,
43.5899784608864,44.0819053518551,44.5738322428237,45.0657591337924,45.557686024761,
46.0496129157297,46.5415398066983,47.033466697667,47.5253935886356,48.0173204796042,
48.5092473705729,49.0011742615415,49.4931011525102,49.9850280434788,50.4769549344475,
50.9688818254161,51.4608087163848,51.9527356073534,52.4446624983221,52.9365893892907,
53.4285162802594,53.920443171228,54.4123700621967,54.9042969531653,55.396223844134,
55.8881507351026),.UNSPECIFIED.);
#554=FACE_BOUND('',#3500,.T.);
#555=FACE_BOUND('',#3515,.T.);
#556=FACE_BOUND('',#3524,.T.);
#557=FACE_BOUND('',#3526,.T.);
#966=PLANE('',#16688);
#967=PLANE('',#16689);
#968=PLANE('',#16690);
#969=PLANE('',#16691);
#970=PLANE('',#16692);
#971=PLANE('',#16693);
#972=PLANE('',#16694);
#973=PLANE('',#16695);
#974=PLANE('',#16696);
#975=PLANE('',#16697);
#976=PLANE('',#16698);
#977=PLANE('',#16699);
#978=PLANE('',#16700);
#979=PLANE('',#16701);
#980=PLANE('',#16702);
#981=PLANE('',#16703);
#982=PLANE('',#16704);
#983=PLANE('',#16705);
#984=PLANE('',#16706);
#985=PLANE('',#16707);
#986=PLANE('',#16708);
#987=PLANE('',#16709);
#988=PLANE('',#16710);
#989=PLANE('',#16711);
#990=PLANE('',#16712);
#991=PLANE('',#16713);
#992=PLANE('',#16714);
#993=PLANE('',#16715);
#994=PLANE('',#16716);
#995=PLANE('',#16717);
#996=PLANE('',#16718);
#997=PLANE('',#16719);
#998=PLANE('',#16724);
#999=PLANE('',#16727);
#1000=PLANE('',#16728);
#1001=PLANE('',#16729);
#1002=PLANE('',#16730);
#1003=PLANE('',#16731);
#1004=PLANE('',#16732);
#1005=PLANE('',#16733);
#1006=PLANE('',#16734);
#1007=PLANE('',#16736);
#1008=PLANE('',#16740);
#1331=B_SPLINE_CURVE_WITH_KNOTS('',3,(#36164,#36165,#36166,#36167,#36168,
#36169,#36170,#36171,#36172,#36173,#36174,#36175,#36176,#36177,#36178,#36179),
 .UNSPECIFIED.,.F.,.F.,(4,3,3,3,3,4),(-4.09323272002467,-3.93541512774918,
-3.44348823678054,-2.95156134581189,-2.45963445484324,-2.07135887395547),
 .UNSPECIFIED.);
#1332=B_SPLINE_CURVE_WITH_KNOTS('',3,(#36182,#36183,#36184,#36185,#36186,
#36187,#36188,#36189,#36190,#36191),.UNSPECIFIED.,.F.,.F.,(4,3,3,4),(0.,
0.491926890968645,0.983853781937294,1.11971880752057),.UNSPECIFIED.);
#1333=B_SPLINE_CURVE_WITH_KNOTS('',3,(#36196,#36197,#36198,#36199,#36200,
#36201,#36202,#36203,#36204,#36205,#36206,#36207,#36208,#36209,#36210,#36211,
#36212,#36213,#36214,#36215,#36216,#36217,#36218,#36219,#36220,#36221,#36222,
#36223,#36224,#36225,#36226,#36227,#36228,#36229,#36230,#36231,#36232,#36233,
#36234,#36235,#36236,#36237,#36238),.UNSPECIFIED.,.F.,.F.,(4,3,3,3,3,3,
3,3,3,3,3,3,3,3,4),(-10.3764180272043,-10.3304647103416,-9.83853781937297,
-9.34661092840432,-8.85468403743567,-8.36275714646702,-7.87083025549837,
-7.37890336452973,-6.88697647356108,-6.39504958259243,-5.90312269162378,
-5.41119580065513,-4.91926890968648,-4.42734201871783,-4.09323272002467),
 .UNSPECIFIED.);
#1334=B_SPLINE_CURVE_WITH_KNOTS('',3,(#36239,#36240,#36241,#36242,#36243,
#36244,#36245,#36246,#36247,#36248,#36249,#36250,#36251,#36252,#36253,#36254,
#36255,#36256,#36257,#36258,#36259,#36260,#36261,#36262,#36263,#36264,#36265,
#36266,#36267,#36268,#36269,#36270,#36271,#36272,#36273,#36274,#36275,#36276,
#36277,#36278,#36279,#36280,#36281),.UNSPECIFIED.,.F.,.F.,(4,3,3,3,3,3,
3,3,3,3,3,3,3,3,4),(1.11971880752057,1.47578067290594,1.96770756387459,
2.45963445484324,2.95156134581189,3.44348823678054,3.93541512774919,4.42734201871784,
4.91926890968648,5.41119580065513,5.90312269162378,6.39504958259243,6.88697647356108,
7.37890336452973,7.40290411470015),.UNSPECIFIED.);
#1335=B_SPLINE_CURVE_WITH_KNOTS('',3,(#36286,#36287,#36288,#36289,#36290,
#36291,#36292,#36293,#36294,#36295,#36296,#36297,#36298,#36299,#36300,#36301,
#36302,#36303,#36304,#36305,#36306,#36307,#36308,#36309,#36310,#36311,#36312,
#36313,#36314,#36315,#36316,#36317,#36318,#36319,#36320,#36321,#36322,#36323,
#36324,#36325),.UNSPECIFIED.,.F.,.F.,(4,3,3,3,3,3,3,3,3,3,3,3,3,4),(-16.6596033343838,
-16.2335874019654,-15.7416605109967,-15.2497336200281,-14.7578067290594,
-14.2658798380908,-13.7739529471221,-13.2820260561535,-12.7900991651849,
-12.2981722742162,-11.8062453832476,-11.3143184922789,-10.8223916013103,
-10.3764180272043),.UNSPECIFIED.);
#1336=B_SPLINE_CURVE_WITH_KNOTS('',3,(#36326,#36327,#36328,#36329,#36330,
#36331,#36332,#36333,#36334,#36335,#36336,#36337,#36338,#36339,#36340,#36341,
#36342,#36343,#36344,#36345,#36346,#36347,#36348,#36349,#36350,#36351,#36352,
#36353,#36354,#36355,#36356,#36357,#36358,#36359,#36360,#36361,#36362,#36363,
#36364,#36365),.UNSPECIFIED.,.F.,.F.,(4,3,3,3,3,3,3,3,3,3,3,3,3,4),(7.40290411470015,
7.87083025549838,8.36275714646703,8.85468403743567,9.34661092840432,9.83853781937297,
10.3304647103416,10.8223916013103,11.3143184922789,11.8062453832476,12.2981722742162,
12.7900991651849,13.2820260561535,13.6860894218797),.UNSPECIFIED.);
#1337=B_SPLINE_CURVE_WITH_KNOTS('',3,(#36370,#36371,#36372,#36373,#36374,
#36375,#36376,#36377,#36378,#36379,#36380,#36381,#36382,#36383,#36384,#36385,
#36386,#36387,#36388,#36389,#36390,#36391,#36392,#36393,#36394,#36395,#36396,
#36397,#36398,#36399,#36400,#36401,#36402,#36403,#36404,#36405,#36406,#36407,
#36408,#36409,#36410,#36411,#36412),.UNSPECIFIED.,.F.,.F.,(4,3,3,3,3,3,
3,3,3,3,3,3,3,3,4),(-22.9427886415634,-22.6286369845578,-22.1367100935892,
-21.6447832026205,-21.1528563116519,-20.6609294206832,-20.1690025297146,
-19.6770756387459,-19.1851487477773,-18.6932218568086,-18.20129496584,-17.7093680748713,
-17.2174411839027,-16.725514292934,-16.6596033343838),.UNSPECIFIED.);
#1338=B_SPLINE_CURVE_WITH_KNOTS('',3,(#36413,#36414,#36415,#36416,#36417,
#36418,#36419,#36420,#36421,#36422,#36423,#36424,#36425,#36426,#36427,#36428,
#36429,#36430,#36431,#36432,#36433,#36434,#36435,#36436,#36437,#36438,#36439,
#36440,#36441,#36442,#36443,#36444,#36445,#36446,#36447,#36448,#36449,#36450,
#36451,#36452,#36453,#36454,#36455),.UNSPECIFIED.,.F.,.F.,(4,3,3,3,3,3,
3,3,3,3,3,3,3,3,4),(13.6860894218797,13.7739529471222,14.2658798380908,
14.7578067290594,15.2497336200281,15.7416605109967,16.2335874019654,16.725514292934,
17.2174411839027,17.7093680748713,18.20129496584,18.6932218568086,19.1851487477773,
19.6770756387459,19.9692747290593),.UNSPECIFIED.);
#1339=B_SPLINE_CURVE_WITH_KNOTS('',3,(#36460,#36461,#36462,#36463,#36464,
#36465,#36466,#36467,#36468,#36469,#36470,#36471,#36472,#36473,#36474,#36475,
#36476,#36477,#36478,#36479,#36480,#36481,#36482,#36483,#36484,#36485,#36486,
#36487,#36488,#36489,#36490,#36491,#36492,#36493,#36494,#36495,#36496,#36497,
#36498,#36499,#36500,#36501,#36502),.UNSPECIFIED.,.F.,.F.,(4,3,3,3,3,3,
3,3,3,3,3,3,3,3,4),(-29.225973948743,-29.0236865671502,-28.5317596761816,
-28.039832785213,-27.5479058942443,-27.0559790032757,-26.564052112307,-26.0721252213384,
-25.5801983303697,-25.0882714394011,-24.5963445484324,-24.1044176574638,
-23.6124907664951,-23.1205638755265,-22.9427886415634),.UNSPECIFIED.);
#1340=B_SPLINE_CURVE_WITH_KNOTS('',3,(#36503,#36504,#36505,#36506,#36507,
#36508,#36509,#36510,#36511,#36512,#36513,#36514,#36515,#36516,#36517,#36518,
#36519,#36520,#36521,#36522,#36523,#36524,#36525,#36526,#36527,#36528,#36529,
#36530,#36531,#36532,#36533,#36534,#36535,#36536,#36537,#36538,#36539,#36540,
#36541,#36542,#36543,#36544,#36545),.UNSPECIFIED.,.F.,.F.,(4,3,3,3,3,3,
3,3,3,3,3,3,3,3,4),(19.9692747290593,20.1690025297146,20.6609294206832,
21.1528563116519,21.6447832026205,22.1367100935892,22.6286369845578,23.1205638755265,
23.6124907664951,24.1044176574638,24.5963445484324,25.0882714394011,25.5801983303697,
26.0721252213384,26.2524600362389),.UNSPECIFIED.);
#1341=B_SPLINE_CURVE_WITH_KNOTS('',3,(#36550,#36551,#36552,#36553,#36554,
#36555,#36556,#36557,#36558,#36559,#36560,#36561,#36562,#36563,#36564,#36565,
#36566,#36567,#36568,#36569,#36570,#36571,#36572,#36573,#36574,#36575,#36576,
#36577,#36578,#36579,#36580,#36581,#36582,#36583,#36584,#36585,#36586,#36587,
#36588,#36589,#36590,#36591,#36592),.UNSPECIFIED.,.F.,.F.,(4,3,3,3,3,3,
3,3,3,3,3,3,3,3,4),(-35.5091592559226,-35.4187361497427,-34.926809258774,
-34.4348823678054,-33.9429554768367,-33.4510285858681,-32.9591016948994,
-32.4671748039308,-31.9752479129621,-31.4833210219935,-30.9913941310248,
-30.4994672400562,-30.0075403490876,-29.5156134581189,-29.225973948743),
 .UNSPECIFIED.);
#1342=B_SPLINE_CURVE_WITH_KNOTS('',3,(#36593,#36594,#36595,#36596,#36597,
#36598,#36599,#36600,#36601,#36602,#36603,#36604,#36605,#36606,#36607,#36608,
#36609,#36610,#36611,#36612,#36613,#36614,#36615,#36616,#36617,#36618,#36619,
#36620,#36621,#36622,#36623,#36624,#36625,#36626,#36627,#36628,#36629,#36630,
#36631,#36632,#36633,#36634,#36635),.UNSPECIFIED.,.F.,.F.,(4,3,3,3,3,3,
3,3,3,3,3,3,3,3,4),(26.2524600362389,26.564052112307,27.0559790032757,27.5479058942443,
28.0398327852129,28.5317596761816,29.0236865671503,29.5156134581189,30.0075403490875,
30.4994672400562,30.9913941310248,31.4833210219935,31.9752479129621,32.4671748039308,
32.5356453434185),.UNSPECIFIED.);
#1343=B_SPLINE_CURVE_WITH_KNOTS('',3,(#36640,#36641,#36642,#36643,#36644,
#36645,#36646,#36647,#36648,#36649,#36650,#36651,#36652,#36653,#36654,#36655,
#36656,#36657,#36658,#36659,#36660,#36661,#36662,#36663,#36664,#36665,#36666,
#36667,#36668,#36669,#36670,#36671,#36672,#36673,#36674,#36675,#36676,#36677,
#36678,#36679),.UNSPECIFIED.,.F.,.F.,(4,3,3,3,3,3,3,3,3,3,3,3,3,4),(-41.7923445631022,
-41.3218588413665,-40.8299319503978,-40.3380050594292,-39.8460781684605,
-39.3541512774919,-38.8622243865232,-38.3702974955546,-37.8783706045859,
-37.3864437136173,-36.8945168226486,-36.40258993168,-35.9106630407113,-35.5091592559226),
 .UNSPECIFIED.);
#1344=B_SPLINE_CURVE_WITH_KNOTS('',3,(#36680,#36681,#36682,#36683,#36684,
#36685,#36686,#36687,#36688,#36689,#36690,#36691,#36692,#36693,#36694,#36695,
#36696,#36697,#36698,#36699,#36700,#36701,#36702,#36703,#36704,#36705,#36706,
#36707,#36708,#36709,#36710,#36711,#36712,#36713,#36714,#36715,#36716,#36717,
#36718,#36719),.UNSPECIFIED.,.F.,.F.,(4,3,3,3,3,3,3,3,3,3,3,3,3,4),(32.5356453434185,
32.9591016948994,33.4510285858681,33.9429554768367,34.4348823678054,34.926809258774,
35.4187361497427,35.9106630407113,36.40258993168,36.8945168226486,37.3864437136173,
37.8783706045859,38.3702974955546,38.8188306505981),.UNSPECIFIED.);
#1345=B_SPLINE_CURVE_WITH_KNOTS('',3,(#36725,#36726,#36727,#36728,#36729),
 .UNSPECIFIED.,.F.,.F.,(4,1,4),(53.4070751110265,53.4285162802594,53.8167918611471),
 .UNSPECIFIED.);
#1346=B_SPLINE_CURVE_WITH_KNOTS('',3,(#36735,#36736,#36737,#36738,#36739,
#36740,#36741,#36742,#36743,#36744,#36745,#36746,#36747,#36748,#36749,#36750),
 .UNSPECIFIED.,.F.,.F.,(4,1,1,1,1,1,1,1,1,1,1,1,1,4),(47.1238898038469,
47.5253935886356,48.0173204796042,48.5092473705729,49.0011742615415,49.4931011525102,
49.9850280434788,50.4769549344475,50.9688818254161,51.4608087163848,51.9527356073534,
52.4446624983221,52.9365893892907,53.4070751110265),.UNSPECIFIED.);
#1347=B_SPLINE_CURVE_WITH_KNOTS('',3,(#36753,#36754,#36755,#36756,#36757,
#36758,#36759,#36760,#36761,#36762,#36763,#36764,#36765,#36766,#36767),
 .UNSPECIFIED.,.F.,.F.,(4,1,1,1,1,1,1,1,1,1,1,1,4),(47.1238898038469,47.167283539772,
47.6592104307407,48.1511373217093,48.6430642126779,49.1349911036466,49.6269179946152,
50.1188448855839,50.6107717765525,51.1026986675212,51.5946255584898,52.0865524494585,
52.5784793404271),.UNSPECIFIED.);
#1348=B_SPLINE_CURVE_WITH_KNOTS('',3,(#36772,#36773,#36774,#36775,#36776,
#36777,#36778,#36779,#36780,#36781,#36782,#36783,#36784,#36785,#36786,#36787,
#36788),.UNSPECIFIED.,.F.,.F.,(4,1,1,1,1,1,1,1,1,1,1,1,1,1,4),(40.8407044966673,
41.1303440060432,41.6222708970118,42.1141977879805,42.6061246789491,43.0980515699178,
43.5899784608864,44.0819053518551,44.5738322428237,45.0657591337924,45.557686024761,
46.0496129157297,46.5415398066983,47.033466697667,47.1238898038469),
 .UNSPECIFIED.);
#1349=B_SPLINE_CURVE_WITH_KNOTS('',3,(#36789,#36790,#36791,#36792,#36793,
#36794,#36795,#36796,#36797,#36798,#36799,#36800,#36801,#36802,#36803,#36804),
 .UNSPECIFIED.,.F.,.F.,(4,1,1,1,1,1,1,1,1,1,1,1,1,4),(40.8407044966673,
41.2641608481482,41.7560877391169,42.2480146300855,42.7399415210542,43.2318684120228,
43.7237953029915,44.2157221939601,44.7076490849288,45.1995759758974,45.6915028668661,
46.1834297578347,46.6753566488034,47.1238898038469),.UNSPECIFIED.);
#1350=B_SPLINE_CURVE_WITH_KNOTS('',3,(#36809,#36810,#36811,#36812,#36813,
#36814,#36815,#36816,#36817,#36818,#36819,#36820,#36821,#36822,#36823,#36824,
#36825),.UNSPECIFIED.,.F.,.F.,(4,1,1,1,1,1,1,1,1,1,1,1,1,1,4),(34.5575191894877,
34.7352944234507,35.2272213144194,35.719148205388,36.2110750963567,36.7030019873253,
37.194928878294,37.6868557692626,38.1787826602313,38.6707095511999,39.1626364421686,
39.6545633331372,40.1464902241059,40.6384171150745,40.8407044966673),
 .UNSPECIFIED.);
#1351=B_SPLINE_CURVE_WITH_KNOTS('',3,(#36826,#36827,#36828,#36829,#36830,
#36831,#36832,#36833,#36834,#36835,#36836,#36837,#36838,#36839,#36840,#36841,
#36842),.UNSPECIFIED.,.F.,.F.,(4,1,1,1,1,1,1,1,1,1,1,1,1,1,4),(34.5575191894877,
34.8691112655558,35.3610381565244,35.8529650474931,36.3448919384617,36.8368188294304,
37.328745720399,37.8206726113677,38.3125995023363,38.804526393305,39.2964532842736,
39.7883801752423,40.2803070662109,40.7722339571796,40.8407044966673),
 .UNSPECIFIED.);
#1352=B_SPLINE_CURVE_WITH_KNOTS('',3,(#36847,#36848,#36849,#36850,#36851,
#36852,#36853,#36854,#36855,#36856,#36857,#36858,#36859,#36860,#36861,#36862,
#36863),.UNSPECIFIED.,.F.,.F.,(4,1,1,1,1,1,1,1,1,1,1,1,1,1,4),(28.2743338823081,
28.3402448408583,28.832171731827,29.3240986227956,29.8160255137643,30.3079524047329,
30.7998792957016,31.2918061866702,31.7837330776389,32.2756599686075,32.7675868595761,
33.2595137505448,33.7514406415134,34.2433675324821,34.5575191894877),
 .UNSPECIFIED.);
#1353=B_SPLINE_CURVE_WITH_KNOTS('',3,(#36864,#36865,#36866,#36867,#36868,
#36869,#36870,#36871,#36872,#36873,#36874,#36875,#36876,#36877,#36878,#36879,
#36880),.UNSPECIFIED.,.F.,.F.,(4,1,1,1,1,1,1,1,1,1,1,1,1,1,4),(28.2743338823081,
28.4740616829634,28.965988573932,29.4579154649007,29.9498423558693,30.441769246838,
30.9336961378066,31.4256230287753,31.9175499197439,32.4094768107125,32.9014037016812,
33.3933305926498,33.8852574836185,34.3771843745871,34.5575191894877),
 .UNSPECIFIED.);
#1354=B_SPLINE_CURVE_WITH_KNOTS('',3,(#36885,#36886,#36887,#36888,#36889,
#36890,#36891,#36892,#36893,#36894,#36895,#36896,#36897,#36898,#36899,#36900),
 .UNSPECIFIED.,.F.,.F.,(4,1,1,1,1,1,1,1,1,1,1,1,1,4),(21.9911485751285,
22.4371221492345,22.9290490402032,23.4209759311718,23.9129028221405,24.4048297131091,
24.8967566040778,25.3886834950464,25.8806103860151,26.3725372769837,26.8644641679524,
27.356391058921,27.8483179498897,28.2743338823081),.UNSPECIFIED.);
#1355=B_SPLINE_CURVE_WITH_KNOTS('',3,(#36901,#36902,#36903,#36904,#36905,
#36906,#36907,#36908,#36909,#36910,#36911,#36912,#36913,#36914,#36915,#36916,
#36917),.UNSPECIFIED.,.F.,.F.,(4,1,1,1,1,1,1,1,1,1,1,1,1,1,4),(21.9911485751285,
22.0790121003709,22.5709389913396,23.0628658823082,23.5547927732769,24.0467196642455,
24.5386465552142,25.0305734461828,25.5225003371515,26.0144272281201,26.5063541190888,
26.9982810100574,27.4902079010261,27.9821347919947,28.2743338823081),
 .UNSPECIFIED.);
#1356=B_SPLINE_CURVE_WITH_KNOTS('',3,(#36922,#36923,#36924,#36925,#36926,
#36927,#36928,#36929,#36930,#36931,#36932,#36933,#36934,#36935,#36936,#36937,
#36938),.UNSPECIFIED.,.F.,.F.,(4,1,1,1,1,1,1,1,1,1,1,1,1,1,4),(15.707963267949,
16.0420725666421,16.5339994576108,17.0259263485794,17.5178532395481,18.0097801305167,
18.5017070214854,18.993633912454,19.4855608034226,19.9774876943913,20.4694145853599,
20.9613414763286,21.4532683672972,21.9451952582659,21.9911485751285),
 .UNSPECIFIED.);
#1357=B_SPLINE_CURVE_WITH_KNOTS('',3,(#36939,#36940,#36941,#36942,#36943,
#36944,#36945,#36946,#36947,#36948,#36949,#36950,#36951,#36952,#36953,#36954),
 .UNSPECIFIED.,.F.,.F.,(4,1,1,1,1,1,1,1,1,1,1,1,1,4),(15.707963267949,16.1758894087472,
16.6678162997158,17.1597431906845,17.6516700816531,18.1435969726218,18.6355238635904,
19.127450754559,19.6193776455277,20.1113045364963,20.603231427465,21.0951583184336,
21.5870852094023,21.9911485751285),.UNSPECIFIED.);
#1358=B_SPLINE_CURVE_WITH_KNOTS('',3,(#37481,#37482,#37483,#37484,#37485,
#37486,#37487,#37488,#37489,#37490,#37491,#37492,#37493,#37494,#37495,#37496,
#37497,#37498,#37499,#37500,#37501,#37502,#37503,#37504,#37505,#37506,#37507,
#37508,#37509,#37510,#37511,#37512,#37513,#37514,#37515,#37516,#37517,#37518,
#37519,#37520,#37521,#37522,#37523,#37524,#37525,#37526,#37527,#37528,#37529,
#37530,#37531,#37532,#37533,#37534,#37535,#37536,#37537,#37538,#37539,#37540,
#37541,#37542,#37543,#37544,#37545,#37546,#37547,#37548,#37549,#37550,#37551,
#37552,#37553,#37554,#37555,#37556,#37557,#37558,#37559,#37560,#37561,#37562,
#37563,#37564,#37565,#37566,#37567,#37568,#37569,#37570,#37571,#37572,#37573,
#37574,#37575,#37576,#37577,#37578,#37579,#37580,#37581,#37582,#37583,#37584,
#37585,#37586,#37587,#37588,#37589,#37590,#37591,#37592,#37593,#37594,#37595,
#37596,#37597,#37598),.UNSPECIFIED.,.F.,.F.,(4,3,3,3,3,3,3,3,3,3,3,3,3,
3,3,3,3,3,3,3,3,3,3,3,3,3,3,3,3,3,3,3,3,3,3,3,3,3,3,4),(0.,0.0681857667088079,
0.0925871972677255,0.160754560978,0.229084940791933,0.297028988213498,0.325731824200965,
0.342177528396621,0.350245710075725,0.417566470176956,0.484648475094958,
0.526651676113238,0.594048569610555,0.661059854099412,0.682534064088732,
0.689876659026608,0.756288907596956,0.822720771296585,0.888378842570404,
0.950859935385141,1.0026277091569,1.01408476217981,1.0221657938941,1.08723429368861,
1.15277237209404,1.2180345613585,1.2826596930891,1.32383090932414,1.34242463013063,
1.34972676639674,1.36500212555917,1.4295571391601,1.49431742045731,1.5286172236547,
1.55554269307663,1.56437072923404,1.62845754216276,1.69224411523009,1.75508079497207,
1.76871584603644),.UNSPECIFIED.);
#1359=B_SPLINE_CURVE_WITH_KNOTS('',3,(#37599,#37600,#37601,#37602,#37603,
#37604,#37605,#37606,#37607,#37608,#37609,#37610,#37611,#37612,#37613,#37614,
#37615,#37616,#37617,#37618,#37619,#37620,#37621,#37622,#37623),
 .UNSPECIFIED.,.F.,.F.,(4,3,3,3,3,3,3,3,4),(38.8188306505981,38.8622243865232,
39.3541512774919,39.8460781684605,40.3380050594292,40.8299319503978,41.3218588413664,
41.8137857323351,42.2020613132229),.UNSPECIFIED.);
#1360=B_SPLINE_CURVE_WITH_KNOTS('',3,(#37625,#37626,#37627,#37628,#37629,
#37630,#37631,#37632,#37633,#37634,#37635,#37636,#37637,#37638,#37639,#37640,
#37641,#37642,#37643,#37644,#37645,#37646,#37647,#37648,#37649,#37650,#37651,
#37652,#37653,#37654,#37655,#37656,#37657,#37658,#37659,#37660,#37661,#37662,
#37663,#37664,#37665,#37666,#37667,#37668,#37669,#37670,#37671,#37672,#37673,
#37674,#37675,#37676,#37677,#37678,#37679,#37680,#37681,#37682,#37683,#37684,
#37685,#37686,#37687,#37688,#37689,#37690,#37691,#37692,#37693,#37694,#37695,
#37696,#37697,#37698,#37699,#37700,#37701,#37702,#37703,#37704,#37705,#37706,
#37707,#37708,#37709,#37710,#37711,#37712,#37713,#37714,#37715,#37716,#37717,
#37718,#37719,#37720,#37721,#37722,#37723,#37724,#37725,#37726,#37727,#37728,
#37729,#37730,#37731,#37732,#37733,#37734,#37735,#37736,#37737,#37738,#37739,
#37740,#37741,#37742),.UNSPECIFIED.,.F.,.F.,(4,3,3,3,3,3,3,3,3,3,3,3,3,
3,3,3,3,3,3,3,3,3,3,3,3,3,3,3,3,3,3,3,3,3,3,3,3,3,3,4),(-1.76871584603644,
-1.7046191062269,-1.68449640386893,-1.62078305031798,-1.57802061157228,
-1.56415526706134,-1.55145880098442,-1.48728260043853,-1.42252268550912,
-1.35794028991274,-1.34735547013984,-1.33863647768557,-1.27868354035241,
-1.21410507385394,-1.1488154291139,-1.0832642762627,-1.02800537889021,-1.01727641030729,
-1.01007836604066,-0.943992267869414,-0.877500202546595,-0.862228686772767,
-0.796068266380696,-0.729641340063069,-0.692925580960443,-0.684965546630163,
-0.676965689034107,-0.610055994476737,-0.542706920162068,-0.475452030986818,
-0.435915267242059,-0.381425858836801,-0.357586742659501,-0.345662846640054,
-0.337975416418596,-0.270932245595006,-0.202736527078763,-0.134396883544413,
-0.0666964856366526,0.),.UNSPECIFIED.);
#1361=B_SPLINE_CURVE_WITH_KNOTS('',3,(#37743,#37744,#37745,#37746,#37747,
#37748,#37749,#37750,#37751,#37752,#37753,#37754,#37755,#37756,#37757),
 .UNSPECIFIED.,.F.,.F.,(4,1,1,1,1,1,1,1,1,1,1,1,4),(10.3764180272043,10.764693608092,
11.2566204990607,11.7485473900293,12.240474280998,12.7324011719666,13.2243280629353,
13.7162549539039,14.2081818448726,14.7001087358412,15.1920356268099,15.6839625177785,
15.707963267949),.UNSPECIFIED.);
#1362=B_SPLINE_CURVE_WITH_KNOTS('',3,(#37763,#37764,#37765,#37766,#37767,
#37768,#37769,#37770,#37771,#37772,#37773,#37774,#37775,#37776,#37777,#37778,
#37779,#37780,#37781,#37782,#37783,#37784,#37785,#37786,#37787,#37788,#37789,
#37790,#37791,#37792,#37793,#37794,#37795,#37796,#37797,#37798,#37799,#37800,
#37801,#37802,#37803,#37804,#37805,#37806,#37807,#37808,#37809,#37810,#37811,
#37812,#37813,#37814,#37815,#37816,#37817,#37818,#37819,#37820,#37821,#37822,
#37823,#37824,#37825,#37826,#37827,#37828,#37829,#37830,#37831,#37832,#37833,
#37834,#37835,#37836,#37837,#37838,#37839,#37840,#37841,#37842,#37843,#37844,
#37845,#37846,#37847,#37848,#37849,#37850,#37851,#37852,#37853,#37854,#37855,
#37856,#37857,#37858,#37859,#37860,#37861,#37862,#37863,#37864,#37865,#37866,
#37867,#37868,#37869,#37870,#37871,#37872,#37873,#37874,#37875,#37876,#37877,
#37878,#37879,#37880),.UNSPECIFIED.,.F.,.F.,(4,3,3,3,3,3,3,3,3,3,3,3,3,
3,3,3,3,3,3,3,3,3,3,3,3,3,3,3,3,3,3,3,3,3,3,3,3,3,3,4),(-1.7649800298231,
-1.69695540332944,-1.67264917116808,-1.60436612704894,-1.55886208432468,
-1.54212438356654,-1.52874434765788,-1.46113379154541,-1.39371142439958,
-1.3268905026446,-1.31426180337642,-1.30254148063391,-1.24033378525489,
-1.17363505650255,-1.10665338574218,-1.03993414154976,-0.984208628543281,
-0.973017916201771,-0.965501098295893,-0.899548822784076,-0.833828509597175,
-0.817032089523831,-0.75098473138995,-0.685204529665416,-0.64999272147509,
-0.642150879902158,-0.634554921790819,-0.569503767261871,-0.504475361186555,
-0.44018015634379,-0.403510064142809,-0.353071306124958,-0.331004349492148,
-0.318701140225958,-0.310509349318208,-0.246725154889164,-0.182546014491394,
-0.118678891385951,-0.0559773875632533,0.),.UNSPECIFIED.);
#1363=B_SPLINE_CURVE_WITH_KNOTS('',3,(#37883,#37884,#37885,#37886,#37887,
#37888,#37889,#37890,#37891,#37892,#37893,#37894),.UNSPECIFIED.,.F.,.F.,
(4,1,1,1,1,1,1,1,1,4),(11.6147305479243,12.1066574388929,12.5985843298616,
13.0905112208302,13.5824381117989,14.0743650027675,14.5662918937362,15.0582187847048,
15.5501456756735,15.707963267949),.UNSPECIFIED.);
#1364=B_SPLINE_CURVE_WITH_KNOTS('',3,(#38268,#38269,#38270,#38271,#38272,
#38273,#38274,#38275,#38276,#38277,#38278,#38279,#38280,#38281,#38282,#38283,
#38284,#38285,#38286,#38287,#38288,#38289,#38290,#38291,#38292,#38293,#38294,
#38295,#38296,#38297,#38298,#38299,#38300,#38301,#38302,#38303,#38304,#38305,
#38306,#38307,#38308,#38309,#38310,#38311,#38312,#38313,#38314,#38315,#38316,
#38317,#38318,#38319,#38320,#38321,#38322,#38323,#38324,#38325,#38326,#38327,
#38328,#38329,#38330,#38331,#38332,#38333,#38334,#38335,#38336,#38337,#38338,
#38339,#38340,#38341,#38342,#38343,#38344,#38345,#38346,#38347,#38348,#38349,
#38350,#38351,#38352,#38353,#38354,#38355,#38356,#38357,#38358,#38359,#38360,
#38361,#38362,#38363,#38364,#38365,#38366,#38367,#38368,#38369,#38370,#38371,
#38372,#38373,#38374,#38375,#38376,#38377,#38378,#38379,#38380,#38381,#38382,
#38383,#38384,#38385),.UNSPECIFIED.,.F.,.F.,(4,3,3,3,3,3,3,3,3,3,3,3,3,
3,3,3,3,3,3,3,3,3,3,3,3,3,3,3,3,3,3,3,3,3,3,3,3,3,3,4),(0.,0.0639852145080714,
0.0841315994229438,0.147534957977308,0.211548544081093,0.275702344548213,
0.302478627892936,0.313393109737379,0.322947639997341,0.387624471507211,
0.452753158889431,0.489912611305994,0.554799697618439,0.59863435069713,
0.636989672140985,0.646993091751658,0.712495556481525,0.778459230466718,
0.844342605144468,0.905476922247968,0.958616291747051,0.969438383973272,
0.97699070665728,1.04256627278548,1.10903071984032,1.17600606522964,1.24274532490853,
1.28666860157458,1.30107863274988,1.30945456030415,1.33059187824063,1.39733368263577,
1.46475749791685,1.50228531440513,1.53103728641692,1.54149218732251,1.60963039313057,
1.6779332296461,1.74577594078118,1.76498002982309),.UNSPECIFIED.);
#1365=B_SPLINE_CURVE_WITH_KNOTS('',3,(#38386,#38387,#38388,#38389,#38390,
#38391,#38392,#38393,#38394,#38395,#38396,#38397,#38398,#38399,#38400,#38401,
#38402,#38403,#38404),.UNSPECIFIED.,.F.,.F.,(4,3,3,3,3,3,4),(-44.2734201871783,
-43.7814932962097,-43.289566405241,-42.7976395142724,-42.3057126233038,
-41.8137857323351,-41.7923445631022),.UNSPECIFIED.);
#1599=CYLINDRICAL_SURFACE('',#16671,8.925);
#1600=CYLINDRICAL_SURFACE('',#16673,8.925);
#1601=CYLINDRICAL_SURFACE('',#16674,8.925);
#1602=CYLINDRICAL_SURFACE('',#16675,8.925);
#1603=CYLINDRICAL_SURFACE('',#16676,8.925);
#1604=CYLINDRICAL_SURFACE('',#16677,8.925);
#1605=CYLINDRICAL_SURFACE('',#16678,8.925);
#1606=CYLINDRICAL_SURFACE('',#16679,8.0685);
#1607=CYLINDRICAL_SURFACE('',#16681,8.0685);
#1608=CYLINDRICAL_SURFACE('',#16683,8.0685);
#1609=CYLINDRICAL_SURFACE('',#16684,8.0685);
#1610=CYLINDRICAL_SURFACE('',#16685,8.0685);
#1611=CYLINDRICAL_SURFACE('',#16686,8.0685);
#1612=CYLINDRICAL_SURFACE('',#16687,8.0685);
#1613=CYLINDRICAL_SURFACE('',#16723,8.0685);
#1614=CYLINDRICAL_SURFACE('',#16739,12.5);
#1615=CYLINDRICAL_SURFACE('',#16743,8.925);
#1616=CYLINDRICAL_SURFACE('',#16744,8.);
#2440=FACE_OUTER_BOUND('',#3464,.T.);
#2441=FACE_OUTER_BOUND('',#3465,.T.);
#2442=FACE_OUTER_BOUND('',#3466,.T.);
#2443=FACE_OUTER_BOUND('',#3467,.T.);
#2444=FACE_OUTER_BOUND('',#3468,.T.);
#2445=FACE_OUTER_BOUND('',#3469,.T.);
#2446=FACE_OUTER_BOUND('',#3470,.T.);
#2447=FACE_OUTER_BOUND('',#3471,.T.);
#2448=FACE_OUTER_BOUND('',#3472,.T.);
#2449=FACE_OUTER_BOUND('',#3473,.T.);
#2450=FACE_OUTER_BOUND('',#3474,.T.);
#2451=FACE_OUTER_BOUND('',#3475,.T.);
#2452=FACE_OUTER_BOUND('',#3476,.T.);
#2453=FACE_OUTER_BOUND('',#3477,.T.);
#2454=FACE_OUTER_BOUND('',#3478,.T.);
#2455=FACE_OUTER_BOUND('',#3479,.T.);
#2456=FACE_OUTER_BOUND('',#3480,.T.);
#2457=FACE_OUTER_BOUND('',#3481,.T.);
#2458=FACE_OUTER_BOUND('',#3482,.T.);
#2459=FACE_OUTER_BOUND('',#3483,.T.);
#2460=FACE_OUTER_BOUND('',#3484,.T.);
#2461=FACE_OUTER_BOUND('',#3485,.T.);
#2462=FACE_OUTER_BOUND('',#3486,.T.);
#2463=FACE_OUTER_BOUND('',#3487,.T.);
#2464=FACE_OUTER_BOUND('',#3488,.T.);
#2465=FACE_OUTER_BOUND('',#3489,.T.);
#2466=FACE_OUTER_BOUND('',#3490,.T.);
#2467=FACE_OUTER_BOUND('',#3491,.T.);
#2468=FACE_OUTER_BOUND('',#3492,.T.);
#2469=FACE_OUTER_BOUND('',#3493,.T.);
#2470=FACE_OUTER_BOUND('',#3494,.T.);
#2471=FACE_OUTER_BOUND('',#3495,.T.);
#2472=FACE_OUTER_BOUND('',#3496,.T.);
#2473=FACE_OUTER_BOUND('',#3497,.T.);
#2474=FACE_OUTER_BOUND('',#3498,.T.);
#2475=FACE_OUTER_BOUND('',#3499,.T.);
#2476=FACE_OUTER_BOUND('',#3501,.T.);
#2477=FACE_OUTER_BOUND('',#3502,.T.);
#2478=FACE_OUTER_BOUND('',#3503,.T.);
#2479=FACE_OUTER_BOUND('',#3504,.T.);
#2480=FACE_OUTER_BOUND('',#3505,.T.);
#2481=FACE_OUTER_BOUND('',#3506,.T.);
#2482=FACE_OUTER_BOUND('',#3507,.T.);
#2483=FACE_OUTER_BOUND('',#3508,.T.);
#2484=FACE_OUTER_BOUND('',#3509,.T.);
#2485=FACE_OUTER_BOUND('',#3510,.T.);
#2486=FACE_OUTER_BOUND('',#3511,.T.);
#2487=FACE_OUTER_BOUND('',#3512,.T.);
#2488=FACE_OUTER_BOUND('',#3513,.T.);
#2489=FACE_OUTER_BOUND('',#3514,.T.);
#2490=FACE_OUTER_BOUND('',#3516,.T.);
#2491=FACE_OUTER_BOUND('',#3517,.T.);
#2492=FACE_OUTER_BOUND('',#3518,.T.);
#2493=FACE_OUTER_BOUND('',#3519,.T.);
#2494=FACE_OUTER_BOUND('',#3520,.T.);
#2495=FACE_OUTER_BOUND('',#3521,.T.);
#2496=FACE_OUTER_BOUND('',#3522,.T.);
#2497=FACE_OUTER_BOUND('',#3523,.T.);
#2498=FACE_OUTER_BOUND('',#3525,.T.);
#2499=FACE_OUTER_BOUND('',#3527,.T.);
#2500=FACE_OUTER_BOUND('',#3528,.T.);
#2501=FACE_OUTER_BOUND('',#3529,.T.);
#2502=FACE_OUTER_BOUND('',#3530,.T.);
#2503=FACE_OUTER_BOUND('',#3531,.T.);
#3464=EDGE_LOOP('',(#13805,#13806,#13807,#13808));
#3465=EDGE_LOOP('',(#13809,#13810,#13811,#13812));
#3466=EDGE_LOOP('',(#13813,#13814,#13815,#13816));
#3467=EDGE_LOOP('',(#13817,#13818,#13819,#13820));
#3468=EDGE_LOOP('',(#13821,#13822,#13823,#13824));
#3469=EDGE_LOOP('',(#13825,#13826,#13827,#13828));
#3470=EDGE_LOOP('',(#13829,#13830,#13831,#13832));
#3471=EDGE_LOOP('',(#13833,#13834,#13835));
#3472=EDGE_LOOP('',(#13836,#13837,#13838,#13839,#13840));
#3473=EDGE_LOOP('',(#13841,#13842,#13843,#13844));
#3474=EDGE_LOOP('',(#13845,#13846,#13847,#13848));
#3475=EDGE_LOOP('',(#13849,#13850,#13851,#13852));
#3476=EDGE_LOOP('',(#13853,#13854,#13855,#13856));
#3477=EDGE_LOOP('',(#13857,#13858,#13859,#13860));
#3478=EDGE_LOOP('',(#13861,#13862,#13863));
#3479=EDGE_LOOP('',(#13864,#13865,#13866,#13867));
#3480=EDGE_LOOP('',(#13868,#13869,#13870));
#3481=EDGE_LOOP('',(#13871,#13872,#13873,#13874));
#3482=EDGE_LOOP('',(#13875,#13876,#13877,#13878));
#3483=EDGE_LOOP('',(#13879,#13880,#13881));
#3484=EDGE_LOOP('',(#13882,#13883,#13884,#13885));
#3485=EDGE_LOOP('',(#13886,#13887,#13888));
#3486=EDGE_LOOP('',(#13889,#13890,#13891,#13892));
#3487=EDGE_LOOP('',(#13893,#13894,#13895,#13896));
#3488=EDGE_LOOP('',(#13897,#13898,#13899));
#3489=EDGE_LOOP('',(#13900,#13901,#13902,#13903));
#3490=EDGE_LOOP('',(#13904,#13905,#13906));
#3491=EDGE_LOOP('',(#13907,#13908,#13909,#13910));
#3492=EDGE_LOOP('',(#13911,#13912,#13913,#13914));
#3493=EDGE_LOOP('',(#13915,#13916,#13917,#13918));
#3494=EDGE_LOOP('',(#13919,#13920,#13921,#13922));
#3495=EDGE_LOOP('',(#13923,#13924,#13925,#13926));
#3496=EDGE_LOOP('',(#13927,#13928,#13929,#13930));
#3497=EDGE_LOOP('',(#13931,#13932,#13933,#13934));
#3498=EDGE_LOOP('',(#13935,#13936,#13937,#13938));
#3499=EDGE_LOOP('',(#13939,#13940,#13941,#13942,#13943,#13944));
#3500=EDGE_LOOP('',(#13945,#13946,#13947,#13948,#13949,#13950));
#3501=EDGE_LOOP('',(#13951,#13952,#13953,#13954));
#3502=EDGE_LOOP('',(#13955,#13956,#13957,#13958));
#3503=EDGE_LOOP('',(#13959,#13960,#13961,#13962));
#3504=EDGE_LOOP('',(#13963,#13964,#13965,#13966));
#3505=EDGE_LOOP('',(#13967,#13968,#13969,#13970));
#3506=EDGE_LOOP('',(#13971,#13972,#13973,#13974));
#3507=EDGE_LOOP('',(#13975,#13976,#13977,#13978));
#3508=EDGE_LOOP('',(#13979,#13980,#13981,#13982));
#3509=EDGE_LOOP('',(#13983,#13984,#13985,#13986));
#3510=EDGE_LOOP('',(#13987,#13988,#13989,#13990,#13991,#13992,#13993,#13994,
#13995,#13996,#13997,#13998,#13999,#14000,#14001,#14002,#14003));
#3511=EDGE_LOOP('',(#14004,#14005,#14006,#14007,#14008));
#3512=EDGE_LOOP('',(#14009,#14010,#14011,#14012));
#3513=EDGE_LOOP('',(#14013,#14014,#14015,#14016,#14017,#14018,#14019,#14020,
#14021,#14022,#14023,#14024,#14025,#14026,#14027,#14028,#14029,#14030));
#3514=EDGE_LOOP('',(#14031,#14032,#14033,#14034,#14035));
#3515=EDGE_LOOP('',(#14036));
#3516=EDGE_LOOP('',(#14037,#14038,#14039,#14040));
#3517=EDGE_LOOP('',(#14041,#14042,#14043,#14044));
#3518=EDGE_LOOP('',(#14045,#14046,#14047,#14048));
#3519=EDGE_LOOP('',(#14049,#14050,#14051,#14052,#14053,#14054));
#3520=EDGE_LOOP('',(#14055,#14056,#14057,#14058));
#3521=EDGE_LOOP('',(#14059,#14060,#14061,#14062));
#3522=EDGE_LOOP('',(#14063,#14064,#14065,#14066));
#3523=EDGE_LOOP('',(#14067));
#3524=EDGE_LOOP('',(#14068,#14069,#14070,#14071,#14072,#14073,#14074,#14075,
#14076,#14077,#14078,#14079));
#3525=EDGE_LOOP('',(#14080));
#3526=EDGE_LOOP('',(#14081));
#3527=EDGE_LOOP('',(#14082,#14083,#14084,#14085));
#3528=EDGE_LOOP('',(#14086));
#3529=EDGE_LOOP('',(#14087,#14088,#14089,#14090,#14091,#14092));
#3530=EDGE_LOOP('',(#14093,#14094,#14095,#14096));
#3531=EDGE_LOOP('',(#14097,#14098,#14099,#14100));
#4500=LINE('',#36162,#5569);
#4501=LINE('',#36195,#5570);
#4502=LINE('',#36285,#5571);
#4503=LINE('',#36369,#5572);
#4504=LINE('',#36459,#5573);
#4505=LINE('',#36549,#5574);
#4506=LINE('',#36639,#5575);
#4507=LINE('',#36723,#5576);
#4508=LINE('',#36734,#5577);
#4509=LINE('',#36771,#5578);
#4510=LINE('',#36808,#5579);
#4511=LINE('',#36846,#5580);
#4512=LINE('',#36884,#5581);
#4513=LINE('',#36921,#5582);
#4514=LINE('',#36958,#5583);
#4515=LINE('',#36960,#5584);
#4516=LINE('',#36961,#5585);
#4517=LINE('',#36965,#5586);
#4518=LINE('',#36966,#5587);
#4519=LINE('',#36967,#5588);
#4520=LINE('',#36971,#5589);
#4521=LINE('',#36973,#5590);
#4522=LINE('',#36974,#5591);
#4523=LINE('',#36978,#5592);
#4524=LINE('',#36979,#5593);
#4525=LINE('',#36980,#5594);
#4526=LINE('',#36982,#5595);
#4527=LINE('',#36983,#5596);
#4528=LINE('',#36987,#5597);
#4529=LINE('',#36989,#5598);
#4530=LINE('',#36990,#5599);
#4531=LINE('',#36994,#5600);
#4532=LINE('',#36995,#5601);
#4533=LINE('',#36996,#5602);
#4534=LINE('',#37000,#5603);
#4535=LINE('',#37002,#5604);
#4536=LINE('',#37003,#5605);
#4537=LINE('',#37007,#5606);
#4538=LINE('',#37008,#5607);
#4539=LINE('',#37009,#5608);
#4540=LINE('',#37011,#5609);
#4541=LINE('',#37012,#5610);
#4542=LINE('',#37016,#5611);
#4543=LINE('',#37018,#5612);
#4544=LINE('',#37019,#5613);
#4545=LINE('',#37023,#5614);
#4546=LINE('',#37024,#5615);
#4547=LINE('',#37025,#5616);
#4548=LINE('',#37029,#5617);
#4549=LINE('',#37031,#5618);
#4550=LINE('',#37032,#5619);
#4551=LINE('',#37036,#5620);
#4552=LINE('',#37037,#5621);
#4553=LINE('',#37038,#5622);
#4554=LINE('',#37040,#5623);
#4555=LINE('',#37041,#5624);
#4556=LINE('',#37043,#5625);
#4557=LINE('',#37044,#5626);
#4558=LINE('',#37046,#5627);
#4559=LINE('',#37047,#5628);
#4560=LINE('',#37049,#5629);
#4561=LINE('',#37050,#5630);
#4562=LINE('',#37052,#5631);
#4563=LINE('',#37054,#5632);
#4564=LINE('',#37056,#5633);
#4565=LINE('',#37060,#5634);
#4566=LINE('',#37062,#5635);
#4567=LINE('',#37064,#5636);
#4568=LINE('',#37066,#5637);
#4569=LINE('',#37068,#5638);
#4570=LINE('',#37069,#5639);
#4571=LINE('',#37072,#5640);
#4572=LINE('',#37074,#5641);
#4573=LINE('',#37075,#5642);
#4574=LINE('',#37078,#5643);
#4575=LINE('',#37079,#5644);
#4576=LINE('',#37082,#5645);
#4577=LINE('',#37084,#5646);
#4578=LINE('',#37085,#5647);
#4579=LINE('',#37088,#5648);
#4580=LINE('',#37089,#5649);
#4581=LINE('',#37091,#5650);
#4582=LINE('',#37093,#5651);
#4583=LINE('',#37096,#5652);
#4584=LINE('',#37098,#5653);
#4585=LINE('',#37099,#5654);
#4586=LINE('',#37102,#5655);
#4587=LINE('',#37103,#5656);
#4588=LINE('',#37106,#5657);
#4589=LINE('',#37107,#5658);
#4590=LINE('',#38411,#5659);
#4591=LINE('',#38412,#5660);
#4592=LINE('',#38415,#5661);
#4593=LINE('',#38416,#5662);
#4594=LINE('',#38418,#5663);
#4595=LINE('',#38421,#5664);
#4596=LINE('',#38423,#5665);
#4597=LINE('',#38425,#5666);
#4598=LINE('',#38435,#5667);
#4599=LINE('',#38440,#5668);
#4600=LINE('',#38443,#5669);
#5569=VECTOR('',#20583,9.);
#5570=VECTOR('',#20588,9.);
#5571=VECTOR('',#20591,9.);
#5572=VECTOR('',#20594,9.);
#5573=VECTOR('',#20597,9.);
#5574=VECTOR('',#20600,9.);
#5575=VECTOR('',#20603,9.);
#5576=VECTOR('',#20606,8.0685);
#5577=VECTOR('',#20611,8.0685);
#5578=VECTOR('',#20616,8.0685);
#5579=VECTOR('',#20619,8.0685);
#5580=VECTOR('',#20622,8.0685);
#5581=VECTOR('',#20625,8.0685);
#5582=VECTOR('',#20628,8.0685);
#5583=VECTOR('',#20631,10.);
#5584=VECTOR('',#20632,10.);
#5585=VECTOR('',#20633,10.);
#5586=VECTOR('',#20636,10.);
#5587=VECTOR('',#20637,10.);
#5588=VECTOR('',#20638,10.);
#5589=VECTOR('',#20641,10.);
#5590=VECTOR('',#20642,10.);
#5591=VECTOR('',#20643,10.);
#5592=VECTOR('',#20646,10.);
#5593=VECTOR('',#20647,10.);
#5594=VECTOR('',#20648,10.);
#5595=VECTOR('',#20651,10.);
#5596=VECTOR('',#20652,10.);
#5597=VECTOR('',#20655,10.);
#5598=VECTOR('',#20656,10.);
#5599=VECTOR('',#20657,10.);
#5600=VECTOR('',#20660,10.);
#5601=VECTOR('',#20661,10.);
#5602=VECTOR('',#20662,10.);
#5603=VECTOR('',#20665,10.);
#5604=VECTOR('',#20666,10.);
#5605=VECTOR('',#20667,10.);
#5606=VECTOR('',#20670,10.);
#5607=VECTOR('',#20671,10.);
#5608=VECTOR('',#20672,10.);
#5609=VECTOR('',#20675,10.);
#5610=VECTOR('',#20676,10.);
#5611=VECTOR('',#20679,10.);
#5612=VECTOR('',#20680,10.);
#5613=VECTOR('',#20681,10.);
#5614=VECTOR('',#20684,10.);
#5615=VECTOR('',#20685,10.);
#5616=VECTOR('',#20686,10.);
#5617=VECTOR('',#20689,10.);
#5618=VECTOR('',#20690,10.);
#5619=VECTOR('',#20691,10.);
#5620=VECTOR('',#20694,10.);
#5621=VECTOR('',#20695,10.);
#5622=VECTOR('',#20696,10.);
#5623=VECTOR('',#20699,10.);
#5624=VECTOR('',#20700,10.);
#5625=VECTOR('',#20703,10.);
#5626=VECTOR('',#20704,10.);
#5627=VECTOR('',#20707,10.);
#5628=VECTOR('',#20708,10.);
#5629=VECTOR('',#20711,10.);
#5630=VECTOR('',#20712,10.);
#5631=VECTOR('',#20715,10.);
#5632=VECTOR('',#20718,10.);
#5633=VECTOR('',#20721,10.);
#5634=VECTOR('',#20724,10.);
#5635=VECTOR('',#20725,10.);
#5636=VECTOR('',#20726,10.);
#5637=VECTOR('',#20727,10.);
#5638=VECTOR('',#20728,10.);
#5639=VECTOR('',#20729,10.);
#5640=VECTOR('',#20732,10.);
#5641=VECTOR('',#20733,10.);
#5642=VECTOR('',#20734,10.);
#5643=VECTOR('',#20737,10.);
#5644=VECTOR('',#20738,10.);
#5645=VECTOR('',#20741,10.);
#5646=VECTOR('',#20742,10.);
#5647=VECTOR('',#20743,10.);
#5648=VECTOR('',#20746,10.);
#5649=VECTOR('',#20747,10.);
#5650=VECTOR('',#20750,10.);
#5651=VECTOR('',#20753,10.);
#5652=VECTOR('',#20756,10.);
#5653=VECTOR('',#20757,10.);
#5654=VECTOR('',#20758,10.);
#5655=VECTOR('',#20761,10.);
#5656=VECTOR('',#20762,10.);
#5657=VECTOR('',#20765,10.);
#5658=VECTOR('',#20766,10.);
#5659=VECTOR('',#20785,10.);
#5660=VECTOR('',#20786,10.);
#5661=VECTOR('',#20789,10.);
#5662=VECTOR('',#20790,10.);
#5663=VECTOR('',#20793,10.);
#5664=VECTOR('',#20798,10.);
#5665=VECTOR('',#20801,10.);
#5666=VECTOR('',#20804,10.);
#5667=VECTOR('',#20817,12.5);
#5668=VECTOR('',#20824,8.75);
#5669=VECTOR('',#20829,8.);
#6259=CIRCLE('',#16672,8.925);
#6260=CIRCLE('',#16680,8.0685);
#6261=CIRCLE('',#16682,8.0685);
#6262=CIRCLE('',#16720,8.925);
#6263=CIRCLE('',#16721,8.925);
#6264=CIRCLE('',#16722,8.0685);
#6265=CIRCLE('',#16725,8.925);
#6266=CIRCLE('',#16726,8.);
#6267=CIRCLE('',#16735,12.5);
#6268=CIRCLE('',#16737,12.5);
#6269=CIRCLE('',#16738,8.);
#6270=CIRCLE('',#16741,8.5);
#7558=VERTEX_POINT('',#36160);
#7559=VERTEX_POINT('',#36161);
#7560=VERTEX_POINT('',#36163);
#7561=VERTEX_POINT('',#36180);
#7562=VERTEX_POINT('',#36193);
#7563=VERTEX_POINT('',#36194);
#7564=VERTEX_POINT('',#36283);
#7565=VERTEX_POINT('',#36284);
#7566=VERTEX_POINT('',#36367);
#7567=VERTEX_POINT('',#36368);
#7568=VERTEX_POINT('',#36457);
#7569=VERTEX_POINT('',#36458);
#7570=VERTEX_POINT('',#36547);
#7571=VERTEX_POINT('',#36548);
#7572=VERTEX_POINT('',#36637);
#7573=VERTEX_POINT('',#36638);
#7574=VERTEX_POINT('',#36721);
#7575=VERTEX_POINT('',#36722);
#7576=VERTEX_POINT('',#36724);
#7577=VERTEX_POINT('',#36732);
#7578=VERTEX_POINT('',#36733);
#7579=VERTEX_POINT('',#36751);
#7580=VERTEX_POINT('',#36769);
#7581=VERTEX_POINT('',#36770);
#7582=VERTEX_POINT('',#36806);
#7583=VERTEX_POINT('',#36807);
#7584=VERTEX_POINT('',#36844);
#7585=VERTEX_POINT('',#36845);
#7586=VERTEX_POINT('',#36882);
#7587=VERTEX_POINT('',#36883);
#7588=VERTEX_POINT('',#36919);
#7589=VERTEX_POINT('',#36920);
#7590=VERTEX_POINT('',#36956);
#7591=VERTEX_POINT('',#36957);
#7592=VERTEX_POINT('',#36959);
#7593=VERTEX_POINT('',#36963);
#7594=VERTEX_POINT('',#36964);
#7595=VERTEX_POINT('',#36969);
#7596=VERTEX_POINT('',#36970);
#7597=VERTEX_POINT('',#36972);
#7598=VERTEX_POINT('',#36976);
#7599=VERTEX_POINT('',#36977);
#7600=VERTEX_POINT('',#36985);
#7601=VERTEX_POINT('',#36986);
#7602=VERTEX_POINT('',#36988);
#7603=VERTEX_POINT('',#36992);
#7604=VERTEX_POINT('',#36993);
#7605=VERTEX_POINT('',#36998);
#7606=VERTEX_POINT('',#36999);
#7607=VERTEX_POINT('',#37001);
#7608=VERTEX_POINT('',#37005);
#7609=VERTEX_POINT('',#37006);
#7610=VERTEX_POINT('',#37014);
#7611=VERTEX_POINT('',#37015);
#7612=VERTEX_POINT('',#37017);
#7613=VERTEX_POINT('',#37021);
#7614=VERTEX_POINT('',#37022);
#7615=VERTEX_POINT('',#37027);
#7616=VERTEX_POINT('',#37028);
#7617=VERTEX_POINT('',#37030);
#7618=VERTEX_POINT('',#37034);
#7619=VERTEX_POINT('',#37035);
#7620=VERTEX_POINT('',#37058);
#7621=VERTEX_POINT('',#37059);
#7622=VERTEX_POINT('',#37061);
#7623=VERTEX_POINT('',#37063);
#7624=VERTEX_POINT('',#37065);
#7625=VERTEX_POINT('',#37067);
#7626=VERTEX_POINT('',#37071);
#7627=VERTEX_POINT('',#37073);
#7628=VERTEX_POINT('',#37077);
#7629=VERTEX_POINT('',#37081);
#7630=VERTEX_POINT('',#37083);
#7631=VERTEX_POINT('',#37087);
#7632=VERTEX_POINT('',#37095);
#7633=VERTEX_POINT('',#37097);
#7634=VERTEX_POINT('',#37101);
#7635=VERTEX_POINT('',#37105);
#7636=VERTEX_POINT('',#37480);
#7637=VERTEX_POINT('',#37624);
#7638=VERTEX_POINT('',#37759);
#7639=VERTEX_POINT('',#37762);
#7640=VERTEX_POINT('',#38267);
#7641=VERTEX_POINT('',#38407);
#7642=VERTEX_POINT('',#38410);
#7643=VERTEX_POINT('',#38414);
#7644=VERTEX_POINT('',#38427);
#7645=VERTEX_POINT('',#38430);
#7646=VERTEX_POINT('',#38432);
#7647=VERTEX_POINT('',#38437);
#9651=EDGE_CURVE('',#7558,#7559,#4500,.T.);
#9652=EDGE_CURVE('',#7558,#7560,#1331,.T.);
#9653=EDGE_CURVE('',#7560,#7561,#6259,.T.);
#9654=EDGE_CURVE('',#7561,#7559,#1332,.T.);
#9655=EDGE_CURVE('',#7562,#7563,#4501,.T.);
#9656=EDGE_CURVE('',#7562,#7558,#1333,.T.);
#9657=EDGE_CURVE('',#7559,#7563,#1334,.T.);
#9658=EDGE_CURVE('',#7564,#7565,#4502,.T.);
#9659=EDGE_CURVE('',#7564,#7562,#1335,.T.);
#9660=EDGE_CURVE('',#7563,#7565,#1336,.T.);
#9661=EDGE_CURVE('',#7566,#7567,#4503,.T.);
#9662=EDGE_CURVE('',#7566,#7564,#1337,.T.);
#9663=EDGE_CURVE('',#7565,#7567,#1338,.T.);
#9664=EDGE_CURVE('',#7568,#7569,#4504,.T.);
#9665=EDGE_CURVE('',#7568,#7566,#1339,.T.);
#9666=EDGE_CURVE('',#7567,#7569,#1340,.T.);
#9667=EDGE_CURVE('',#7570,#7571,#4505,.T.);
#9668=EDGE_CURVE('',#7570,#7568,#1341,.T.);
#9669=EDGE_CURVE('',#7569,#7571,#1342,.T.);
#9670=EDGE_CURVE('',#7572,#7573,#4506,.T.);
#9671=EDGE_CURVE('',#7572,#7570,#1343,.T.);
#9672=EDGE_CURVE('',#7571,#7573,#1344,.T.);
#9673=EDGE_CURVE('',#7574,#7575,#4507,.T.);
#9674=EDGE_CURVE('',#7574,#7576,#1345,.T.);
#9675=EDGE_CURVE('',#7575,#7576,#6260,.T.);
#9676=EDGE_CURVE('',#7577,#7578,#4508,.T.);
#9677=EDGE_CURVE('',#7577,#7574,#1346,.T.);
#9678=EDGE_CURVE('',#7579,#7575,#6261,.T.);
#9679=EDGE_CURVE('',#7578,#7579,#1347,.T.);
#9680=EDGE_CURVE('',#7580,#7581,#4509,.T.);
#9681=EDGE_CURVE('',#7580,#7577,#1348,.T.);
#9682=EDGE_CURVE('',#7581,#7578,#1349,.T.);
#9683=EDGE_CURVE('',#7582,#7583,#4510,.T.);
#9684=EDGE_CURVE('',#7582,#7580,#1350,.T.);
#9685=EDGE_CURVE('',#7583,#7581,#1351,.T.);
#9686=EDGE_CURVE('',#7584,#7585,#4511,.T.);
#9687=EDGE_CURVE('',#7584,#7582,#1352,.T.);
#9688=EDGE_CURVE('',#7585,#7583,#1353,.T.);
#9689=EDGE_CURVE('',#7586,#7587,#4512,.T.);
#9690=EDGE_CURVE('',#7586,#7584,#1354,.T.);
#9691=EDGE_CURVE('',#7587,#7585,#1355,.T.);
#9692=EDGE_CURVE('',#7588,#7589,#4513,.T.);
#9693=EDGE_CURVE('',#7588,#7586,#1356,.T.);
#9694=EDGE_CURVE('',#7589,#7587,#1357,.T.);
#9695=EDGE_CURVE('',#7590,#7591,#4514,.T.);
#9696=EDGE_CURVE('',#7592,#7590,#4515,.T.);
#9697=EDGE_CURVE('',#7591,#7592,#4516,.T.);
#9698=EDGE_CURVE('',#7593,#7594,#4517,.T.);
#9699=EDGE_CURVE('',#7593,#7592,#4518,.T.);
#9700=EDGE_CURVE('',#7590,#7594,#4519,.T.);
#9701=EDGE_CURVE('',#7595,#7596,#4520,.T.);
#9702=EDGE_CURVE('',#7597,#7595,#4521,.T.);
#9703=EDGE_CURVE('',#7596,#7597,#4522,.T.);
#9704=EDGE_CURVE('',#7598,#7599,#4523,.T.);
#9705=EDGE_CURVE('',#7598,#7597,#4524,.T.);
#9706=EDGE_CURVE('',#7595,#7599,#4525,.T.);
#9707=EDGE_CURVE('',#7591,#7596,#4526,.T.);
#9708=EDGE_CURVE('',#7597,#7590,#4527,.T.);
#9709=EDGE_CURVE('',#7600,#7601,#4528,.T.);
#9710=EDGE_CURVE('',#7602,#7600,#4529,.T.);
#9711=EDGE_CURVE('',#7601,#7602,#4530,.T.);
#9712=EDGE_CURVE('',#7603,#7604,#4531,.T.);
#9713=EDGE_CURVE('',#7603,#7602,#4532,.T.);
#9714=EDGE_CURVE('',#7600,#7604,#4533,.T.);
#9715=EDGE_CURVE('',#7605,#7606,#4534,.T.);
#9716=EDGE_CURVE('',#7607,#7605,#4535,.T.);
#9717=EDGE_CURVE('',#7606,#7607,#4536,.T.);
#9718=EDGE_CURVE('',#7608,#7609,#4537,.T.);
#9719=EDGE_CURVE('',#7608,#7607,#4538,.T.);
#9720=EDGE_CURVE('',#7605,#7609,#4539,.T.);
#9721=EDGE_CURVE('',#7596,#7606,#4540,.T.);
#9722=EDGE_CURVE('',#7607,#7595,#4541,.T.);
#9723=EDGE_CURVE('',#7610,#7611,#4542,.T.);
#9724=EDGE_CURVE('',#7612,#7610,#4543,.T.);
#9725=EDGE_CURVE('',#7611,#7612,#4544,.T.);
#9726=EDGE_CURVE('',#7613,#7614,#4545,.T.);
#9727=EDGE_CURVE('',#7613,#7612,#4546,.T.);
#9728=EDGE_CURVE('',#7610,#7614,#4547,.T.);
#9729=EDGE_CURVE('',#7615,#7616,#4548,.T.);
#9730=EDGE_CURVE('',#7617,#7615,#4549,.T.);
#9731=EDGE_CURVE('',#7616,#7617,#4550,.T.);
#9732=EDGE_CURVE('',#7618,#7619,#4551,.T.);
#9733=EDGE_CURVE('',#7618,#7617,#4552,.T.);
#9734=EDGE_CURVE('',#7615,#7619,#4553,.T.);
#9735=EDGE_CURVE('',#7606,#7616,#4554,.T.);
#9736=EDGE_CURVE('',#7617,#7605,#4555,.T.);
#9737=EDGE_CURVE('',#7616,#7611,#4556,.T.);
#9738=EDGE_CURVE('',#7612,#7615,#4557,.T.);
#9739=EDGE_CURVE('',#7611,#7601,#4558,.T.);
#9740=EDGE_CURVE('',#7602,#7610,#4559,.T.);
#9741=EDGE_CURVE('',#7601,#7591,#4560,.T.);
#9742=EDGE_CURVE('',#7592,#7600,#4561,.T.);
#9743=EDGE_CURVE('',#7594,#7598,#4562,.T.);
#9744=EDGE_CURVE('',#7599,#7608,#4563,.T.);
#9745=EDGE_CURVE('',#7609,#7618,#4564,.T.);
#9746=EDGE_CURVE('',#7620,#7621,#4565,.T.);
#9747=EDGE_CURVE('',#7622,#7620,#4566,.T.);
#9748=EDGE_CURVE('',#7623,#7622,#4567,.T.);
#9749=EDGE_CURVE('',#7624,#7623,#4568,.T.);
#9750=EDGE_CURVE('',#7625,#7624,#4569,.T.);
#9751=EDGE_CURVE('',#7621,#7625,#4570,.T.);
#9752=EDGE_CURVE('',#7623,#7626,#4571,.T.);
#9753=EDGE_CURVE('',#7626,#7627,#4572,.T.);
#9754=EDGE_CURVE('',#7624,#7627,#4573,.T.);
#9755=EDGE_CURVE('',#7622,#7628,#4574,.T.);
#9756=EDGE_CURVE('',#7628,#7626,#4575,.T.);
#9757=EDGE_CURVE('',#7621,#7629,#4576,.T.);
#9758=EDGE_CURVE('',#7629,#7630,#4577,.T.);
#9759=EDGE_CURVE('',#7630,#7620,#4578,.T.);
#9760=EDGE_CURVE('',#7631,#7629,#4579,.T.);
#9761=EDGE_CURVE('',#7625,#7631,#4580,.T.);
#9762=EDGE_CURVE('',#7630,#7628,#4581,.T.);
#9763=EDGE_CURVE('',#7627,#7631,#4582,.T.);
#9764=EDGE_CURVE('',#7628,#7632,#4583,.T.);
#9765=EDGE_CURVE('',#7632,#7633,#4584,.T.);
#9766=EDGE_CURVE('',#7626,#7633,#4585,.T.);
#9767=EDGE_CURVE('',#7630,#7634,#4586,.T.);
#9768=EDGE_CURVE('',#7634,#7632,#4587,.T.);
#9769=EDGE_CURVE('',#7629,#7635,#4588,.T.);
#9770=EDGE_CURVE('',#7635,#7634,#4589,.T.);
#9771=EDGE_CURVE('',#7636,#7579,#1358,.T.);
#9772=EDGE_CURVE('',#7573,#7636,#1359,.T.);
#9773=EDGE_CURVE('',#7637,#7561,#1360,.T.);
#9774=EDGE_CURVE('',#7637,#7589,#1361,.T.);
#9775=EDGE_CURVE('',#7561,#7638,#6262,.T.);
#9776=EDGE_CURVE('',#7638,#7560,#6263,.T.);
#9777=EDGE_CURVE('',#7560,#7639,#1362,.T.);
#9778=EDGE_CURVE('',#7639,#7637,#6264,.T.);
#9779=EDGE_CURVE('',#7639,#7588,#1363,.T.);
#9780=EDGE_CURVE('',#7576,#7640,#1364,.T.);
#9781=EDGE_CURVE('',#7640,#7572,#1365,.T.);
#9782=EDGE_CURVE('',#7640,#7636,#6265,.F.);
#9783=EDGE_CURVE('',#7641,#7641,#6266,.T.);
#9784=EDGE_CURVE('',#7631,#7642,#4590,.T.);
#9785=EDGE_CURVE('',#7642,#7635,#4591,.T.);
#9786=EDGE_CURVE('',#7627,#7643,#4592,.T.);
#9787=EDGE_CURVE('',#7643,#7642,#4593,.T.);
#9788=EDGE_CURVE('',#7633,#7643,#4594,.T.);
#9789=EDGE_CURVE('',#7619,#7613,#4595,.T.);
#9790=EDGE_CURVE('',#7614,#7603,#4596,.T.);
#9791=EDGE_CURVE('',#7604,#7593,#4597,.T.);
#9792=EDGE_CURVE('',#7644,#7644,#6267,.T.);
#9793=EDGE_CURVE('',#7645,#7645,#6268,.T.);
#9794=EDGE_CURVE('',#7646,#7646,#6269,.T.);
#9795=EDGE_CURVE('',#7644,#7645,#4598,.T.);
#9796=EDGE_CURVE('',#7647,#7647,#6270,.T.);
#9797=EDGE_CURVE('',#7638,#7647,#4599,.T.);
#9798=EDGE_CURVE('',#7646,#7641,#4600,.T.);
#13805=ORIENTED_EDGE('',*,*,#9651,.F.);
#13806=ORIENTED_EDGE('',*,*,#9652,.T.);
#13807=ORIENTED_EDGE('',*,*,#9653,.T.);
#13808=ORIENTED_EDGE('',*,*,#9654,.T.);
#13809=ORIENTED_EDGE('',*,*,#9655,.F.);
#13810=ORIENTED_EDGE('',*,*,#9656,.T.);
#13811=ORIENTED_EDGE('',*,*,#9651,.T.);
#13812=ORIENTED_EDGE('',*,*,#9657,.T.);
#13813=ORIENTED_EDGE('',*,*,#9658,.F.);
#13814=ORIENTED_EDGE('',*,*,#9659,.T.);
#13815=ORIENTED_EDGE('',*,*,#9655,.T.);
#13816=ORIENTED_EDGE('',*,*,#9660,.T.);
#13817=ORIENTED_EDGE('',*,*,#9661,.F.);
#13818=ORIENTED_EDGE('',*,*,#9662,.T.);
#13819=ORIENTED_EDGE('',*,*,#9658,.T.);
#13820=ORIENTED_EDGE('',*,*,#9663,.T.);
#13821=ORIENTED_EDGE('',*,*,#9664,.F.);
#13822=ORIENTED_EDGE('',*,*,#9665,.T.);
#13823=ORIENTED_EDGE('',*,*,#9661,.T.);
#13824=ORIENTED_EDGE('',*,*,#9666,.T.);
#13825=ORIENTED_EDGE('',*,*,#9667,.F.);
#13826=ORIENTED_EDGE('',*,*,#9668,.T.);
#13827=ORIENTED_EDGE('',*,*,#9664,.T.);
#13828=ORIENTED_EDGE('',*,*,#9669,.T.);
#13829=ORIENTED_EDGE('',*,*,#9670,.F.);
#13830=ORIENTED_EDGE('',*,*,#9671,.T.);
#13831=ORIENTED_EDGE('',*,*,#9667,.T.);
#13832=ORIENTED_EDGE('',*,*,#9672,.T.);
#13833=ORIENTED_EDGE('',*,*,#9673,.F.);
#13834=ORIENTED_EDGE('',*,*,#9674,.T.);
#13835=ORIENTED_EDGE('',*,*,#9675,.F.);
#13836=ORIENTED_EDGE('',*,*,#9676,.F.);
#13837=ORIENTED_EDGE('',*,*,#9677,.T.);
#13838=ORIENTED_EDGE('',*,*,#9673,.T.);
#13839=ORIENTED_EDGE('',*,*,#9678,.F.);
#13840=ORIENTED_EDGE('',*,*,#9679,.F.);
#13841=ORIENTED_EDGE('',*,*,#9680,.F.);
#13842=ORIENTED_EDGE('',*,*,#9681,.T.);
#13843=ORIENTED_EDGE('',*,*,#9676,.T.);
#13844=ORIENTED_EDGE('',*,*,#9682,.F.);
#13845=ORIENTED_EDGE('',*,*,#9683,.F.);
#13846=ORIENTED_EDGE('',*,*,#9684,.T.);
#13847=ORIENTED_EDGE('',*,*,#9680,.T.);
#13848=ORIENTED_EDGE('',*,*,#9685,.F.);
#13849=ORIENTED_EDGE('',*,*,#9686,.F.);
#13850=ORIENTED_EDGE('',*,*,#9687,.T.);
#13851=ORIENTED_EDGE('',*,*,#9683,.T.);
#13852=ORIENTED_EDGE('',*,*,#9688,.F.);
#13853=ORIENTED_EDGE('',*,*,#9689,.F.);
#13854=ORIENTED_EDGE('',*,*,#9690,.T.);
#13855=ORIENTED_EDGE('',*,*,#9686,.T.);
#13856=ORIENTED_EDGE('',*,*,#9691,.F.);
#13857=ORIENTED_EDGE('',*,*,#9692,.F.);
#13858=ORIENTED_EDGE('',*,*,#9693,.T.);
#13859=ORIENTED_EDGE('',*,*,#9689,.T.);
#13860=ORIENTED_EDGE('',*,*,#9694,.F.);
#13861=ORIENTED_EDGE('',*,*,#9695,.F.);
#13862=ORIENTED_EDGE('',*,*,#9696,.F.);
#13863=ORIENTED_EDGE('',*,*,#9697,.F.);
#13864=ORIENTED_EDGE('',*,*,#9698,.F.);
#13865=ORIENTED_EDGE('',*,*,#9699,.T.);
#13866=ORIENTED_EDGE('',*,*,#9696,.T.);
#13867=ORIENTED_EDGE('',*,*,#9700,.T.);
#13868=ORIENTED_EDGE('',*,*,#9701,.F.);
#13869=ORIENTED_EDGE('',*,*,#9702,.F.);
#13870=ORIENTED_EDGE('',*,*,#9703,.F.);
#13871=ORIENTED_EDGE('',*,*,#9704,.F.);
#13872=ORIENTED_EDGE('',*,*,#9705,.T.);
#13873=ORIENTED_EDGE('',*,*,#9702,.T.);
#13874=ORIENTED_EDGE('',*,*,#9706,.T.);
#13875=ORIENTED_EDGE('',*,*,#9695,.T.);
#13876=ORIENTED_EDGE('',*,*,#9707,.T.);
#13877=ORIENTED_EDGE('',*,*,#9703,.T.);
#13878=ORIENTED_EDGE('',*,*,#9708,.T.);
#13879=ORIENTED_EDGE('',*,*,#9709,.F.);
#13880=ORIENTED_EDGE('',*,*,#9710,.F.);
#13881=ORIENTED_EDGE('',*,*,#9711,.F.);
#13882=ORIENTED_EDGE('',*,*,#9712,.F.);
#13883=ORIENTED_EDGE('',*,*,#9713,.T.);
#13884=ORIENTED_EDGE('',*,*,#9710,.T.);
#13885=ORIENTED_EDGE('',*,*,#9714,.T.);
#13886=ORIENTED_EDGE('',*,*,#9715,.F.);
#13887=ORIENTED_EDGE('',*,*,#9716,.F.);
#13888=ORIENTED_EDGE('',*,*,#9717,.F.);
#13889=ORIENTED_EDGE('',*,*,#9718,.F.);
#13890=ORIENTED_EDGE('',*,*,#9719,.T.);
#13891=ORIENTED_EDGE('',*,*,#9716,.T.);
#13892=ORIENTED_EDGE('',*,*,#9720,.T.);
#13893=ORIENTED_EDGE('',*,*,#9701,.T.);
#13894=ORIENTED_EDGE('',*,*,#9721,.T.);
#13895=ORIENTED_EDGE('',*,*,#9717,.T.);
#13896=ORIENTED_EDGE('',*,*,#9722,.T.);
#13897=ORIENTED_EDGE('',*,*,#9723,.F.);
#13898=ORIENTED_EDGE('',*,*,#9724,.F.);
#13899=ORIENTED_EDGE('',*,*,#9725,.F.);
#13900=ORIENTED_EDGE('',*,*,#9726,.F.);
#13901=ORIENTED_EDGE('',*,*,#9727,.T.);
#13902=ORIENTED_EDGE('',*,*,#9724,.T.);
#13903=ORIENTED_EDGE('',*,*,#9728,.T.);
#13904=ORIENTED_EDGE('',*,*,#9729,.F.);
#13905=ORIENTED_EDGE('',*,*,#9730,.F.);
#13906=ORIENTED_EDGE('',*,*,#9731,.F.);
#13907=ORIENTED_EDGE('',*,*,#9732,.F.);
#13908=ORIENTED_EDGE('',*,*,#9733,.T.);
#13909=ORIENTED_EDGE('',*,*,#9730,.T.);
#13910=ORIENTED_EDGE('',*,*,#9734,.T.);
#13911=ORIENTED_EDGE('',*,*,#9715,.T.);
#13912=ORIENTED_EDGE('',*,*,#9735,.T.);
#13913=ORIENTED_EDGE('',*,*,#9731,.T.);
#13914=ORIENTED_EDGE('',*,*,#9736,.T.);
#13915=ORIENTED_EDGE('',*,*,#9729,.T.);
#13916=ORIENTED_EDGE('',*,*,#9737,.T.);
#13917=ORIENTED_EDGE('',*,*,#9725,.T.);
#13918=ORIENTED_EDGE('',*,*,#9738,.T.);
#13919=ORIENTED_EDGE('',*,*,#9723,.T.);
#13920=ORIENTED_EDGE('',*,*,#9739,.T.);
#13921=ORIENTED_EDGE('',*,*,#9711,.T.);
#13922=ORIENTED_EDGE('',*,*,#9740,.T.);
#13923=ORIENTED_EDGE('',*,*,#9709,.T.);
#13924=ORIENTED_EDGE('',*,*,#9741,.T.);
#13925=ORIENTED_EDGE('',*,*,#9697,.T.);
#13926=ORIENTED_EDGE('',*,*,#9742,.T.);
#13927=ORIENTED_EDGE('',*,*,#9700,.F.);
#13928=ORIENTED_EDGE('',*,*,#9708,.F.);
#13929=ORIENTED_EDGE('',*,*,#9705,.F.);
#13930=ORIENTED_EDGE('',*,*,#9743,.F.);
#13931=ORIENTED_EDGE('',*,*,#9706,.F.);
#13932=ORIENTED_EDGE('',*,*,#9722,.F.);
#13933=ORIENTED_EDGE('',*,*,#9719,.F.);
#13934=ORIENTED_EDGE('',*,*,#9744,.F.);
#13935=ORIENTED_EDGE('',*,*,#9720,.F.);
#13936=ORIENTED_EDGE('',*,*,#9736,.F.);
#13937=ORIENTED_EDGE('',*,*,#9733,.F.);
#13938=ORIENTED_EDGE('',*,*,#9745,.F.);
#13939=ORIENTED_EDGE('',*,*,#9707,.F.);
#13940=ORIENTED_EDGE('',*,*,#9741,.F.);
#13941=ORIENTED_EDGE('',*,*,#9739,.F.);
#13942=ORIENTED_EDGE('',*,*,#9737,.F.);
#13943=ORIENTED_EDGE('',*,*,#9735,.F.);
#13944=ORIENTED_EDGE('',*,*,#9721,.F.);
#13945=ORIENTED_EDGE('',*,*,#9746,.F.);
#13946=ORIENTED_EDGE('',*,*,#9747,.F.);
#13947=ORIENTED_EDGE('',*,*,#9748,.F.);
#13948=ORIENTED_EDGE('',*,*,#9749,.F.);
#13949=ORIENTED_EDGE('',*,*,#9750,.F.);
#13950=ORIENTED_EDGE('',*,*,#9751,.F.);
#13951=ORIENTED_EDGE('',*,*,#9749,.T.);
#13952=ORIENTED_EDGE('',*,*,#9752,.T.);
#13953=ORIENTED_EDGE('',*,*,#9753,.T.);
#13954=ORIENTED_EDGE('',*,*,#9754,.F.);
#13955=ORIENTED_EDGE('',*,*,#9748,.T.);
#13956=ORIENTED_EDGE('',*,*,#9755,.T.);
#13957=ORIENTED_EDGE('',*,*,#9756,.T.);
#13958=ORIENTED_EDGE('',*,*,#9752,.F.);
#13959=ORIENTED_EDGE('',*,*,#9746,.T.);
#13960=ORIENTED_EDGE('',*,*,#9757,.T.);
#13961=ORIENTED_EDGE('',*,*,#9758,.T.);
#13962=ORIENTED_EDGE('',*,*,#9759,.T.);
#13963=ORIENTED_EDGE('',*,*,#9760,.T.);
#13964=ORIENTED_EDGE('',*,*,#9757,.F.);
#13965=ORIENTED_EDGE('',*,*,#9751,.T.);
#13966=ORIENTED_EDGE('',*,*,#9761,.T.);
#13967=ORIENTED_EDGE('',*,*,#9747,.T.);
#13968=ORIENTED_EDGE('',*,*,#9759,.F.);
#13969=ORIENTED_EDGE('',*,*,#9762,.T.);
#13970=ORIENTED_EDGE('',*,*,#9755,.F.);
#13971=ORIENTED_EDGE('',*,*,#9763,.T.);
#13972=ORIENTED_EDGE('',*,*,#9761,.F.);
#13973=ORIENTED_EDGE('',*,*,#9750,.T.);
#13974=ORIENTED_EDGE('',*,*,#9754,.T.);
#13975=ORIENTED_EDGE('',*,*,#9756,.F.);
#13976=ORIENTED_EDGE('',*,*,#9764,.T.);
#13977=ORIENTED_EDGE('',*,*,#9765,.T.);
#13978=ORIENTED_EDGE('',*,*,#9766,.F.);
#13979=ORIENTED_EDGE('',*,*,#9762,.F.);
#13980=ORIENTED_EDGE('',*,*,#9767,.T.);
#13981=ORIENTED_EDGE('',*,*,#9768,.T.);
#13982=ORIENTED_EDGE('',*,*,#9764,.F.);
#13983=ORIENTED_EDGE('',*,*,#9758,.F.);
#13984=ORIENTED_EDGE('',*,*,#9769,.T.);
#13985=ORIENTED_EDGE('',*,*,#9770,.T.);
#13986=ORIENTED_EDGE('',*,*,#9767,.F.);
#13987=ORIENTED_EDGE('',*,*,#9771,.F.);
#13988=ORIENTED_EDGE('',*,*,#9772,.F.);
#13989=ORIENTED_EDGE('',*,*,#9672,.F.);
#13990=ORIENTED_EDGE('',*,*,#9669,.F.);
#13991=ORIENTED_EDGE('',*,*,#9666,.F.);
#13992=ORIENTED_EDGE('',*,*,#9663,.F.);
#13993=ORIENTED_EDGE('',*,*,#9660,.F.);
#13994=ORIENTED_EDGE('',*,*,#9657,.F.);
#13995=ORIENTED_EDGE('',*,*,#9654,.F.);
#13996=ORIENTED_EDGE('',*,*,#9773,.F.);
#13997=ORIENTED_EDGE('',*,*,#9774,.T.);
#13998=ORIENTED_EDGE('',*,*,#9694,.T.);
#13999=ORIENTED_EDGE('',*,*,#9691,.T.);
#14000=ORIENTED_EDGE('',*,*,#9688,.T.);
#14001=ORIENTED_EDGE('',*,*,#9685,.T.);
#14002=ORIENTED_EDGE('',*,*,#9682,.T.);
#14003=ORIENTED_EDGE('',*,*,#9679,.T.);
#14004=ORIENTED_EDGE('',*,*,#9775,.T.);
#14005=ORIENTED_EDGE('',*,*,#9776,.T.);
#14006=ORIENTED_EDGE('',*,*,#9777,.T.);
#14007=ORIENTED_EDGE('',*,*,#9778,.T.);
#14008=ORIENTED_EDGE('',*,*,#9773,.T.);
#14009=ORIENTED_EDGE('',*,*,#9692,.T.);
#14010=ORIENTED_EDGE('',*,*,#9774,.F.);
#14011=ORIENTED_EDGE('',*,*,#9778,.F.);
#14012=ORIENTED_EDGE('',*,*,#9779,.T.);
#14013=ORIENTED_EDGE('',*,*,#9780,.F.);
#14014=ORIENTED_EDGE('',*,*,#9674,.F.);
#14015=ORIENTED_EDGE('',*,*,#9677,.F.);
#14016=ORIENTED_EDGE('',*,*,#9681,.F.);
#14017=ORIENTED_EDGE('',*,*,#9684,.F.);
#14018=ORIENTED_EDGE('',*,*,#9687,.F.);
#14019=ORIENTED_EDGE('',*,*,#9690,.F.);
#14020=ORIENTED_EDGE('',*,*,#9693,.F.);
#14021=ORIENTED_EDGE('',*,*,#9779,.F.);
#14022=ORIENTED_EDGE('',*,*,#9777,.F.);
#14023=ORIENTED_EDGE('',*,*,#9652,.F.);
#14024=ORIENTED_EDGE('',*,*,#9656,.F.);
#14025=ORIENTED_EDGE('',*,*,#9659,.F.);
#14026=ORIENTED_EDGE('',*,*,#9662,.F.);
#14027=ORIENTED_EDGE('',*,*,#9665,.F.);
#14028=ORIENTED_EDGE('',*,*,#9668,.F.);
#14029=ORIENTED_EDGE('',*,*,#9671,.F.);
#14030=ORIENTED_EDGE('',*,*,#9781,.F.);
#14031=ORIENTED_EDGE('',*,*,#9771,.T.);
#14032=ORIENTED_EDGE('',*,*,#9678,.T.);
#14033=ORIENTED_EDGE('',*,*,#9675,.T.);
#14034=ORIENTED_EDGE('',*,*,#9780,.T.);
#14035=ORIENTED_EDGE('',*,*,#9782,.T.);
#14036=ORIENTED_EDGE('',*,*,#9783,.F.);
#14037=ORIENTED_EDGE('',*,*,#9760,.F.);
#14038=ORIENTED_EDGE('',*,*,#9784,.T.);
#14039=ORIENTED_EDGE('',*,*,#9785,.T.);
#14040=ORIENTED_EDGE('',*,*,#9769,.F.);
#14041=ORIENTED_EDGE('',*,*,#9763,.F.);
#14042=ORIENTED_EDGE('',*,*,#9786,.T.);
#14043=ORIENTED_EDGE('',*,*,#9787,.T.);
#14044=ORIENTED_EDGE('',*,*,#9784,.F.);
#14045=ORIENTED_EDGE('',*,*,#9753,.F.);
#14046=ORIENTED_EDGE('',*,*,#9766,.T.);
#14047=ORIENTED_EDGE('',*,*,#9788,.T.);
#14048=ORIENTED_EDGE('',*,*,#9786,.F.);
#14049=ORIENTED_EDGE('',*,*,#9768,.F.);
#14050=ORIENTED_EDGE('',*,*,#9770,.F.);
#14051=ORIENTED_EDGE('',*,*,#9785,.F.);
#14052=ORIENTED_EDGE('',*,*,#9787,.F.);
#14053=ORIENTED_EDGE('',*,*,#9788,.F.);
#14054=ORIENTED_EDGE('',*,*,#9765,.F.);
#14055=ORIENTED_EDGE('',*,*,#9727,.F.);
#14056=ORIENTED_EDGE('',*,*,#9789,.F.);
#14057=ORIENTED_EDGE('',*,*,#9734,.F.);
#14058=ORIENTED_EDGE('',*,*,#9738,.F.);
#14059=ORIENTED_EDGE('',*,*,#9713,.F.);
#14060=ORIENTED_EDGE('',*,*,#9790,.F.);
#14061=ORIENTED_EDGE('',*,*,#9728,.F.);
#14062=ORIENTED_EDGE('',*,*,#9740,.F.);
#14063=ORIENTED_EDGE('',*,*,#9699,.F.);
#14064=ORIENTED_EDGE('',*,*,#9791,.F.);
#14065=ORIENTED_EDGE('',*,*,#9714,.F.);
#14066=ORIENTED_EDGE('',*,*,#9742,.F.);
#14067=ORIENTED_EDGE('',*,*,#9792,.T.);
#14068=ORIENTED_EDGE('',*,*,#9698,.T.);
#14069=ORIENTED_EDGE('',*,*,#9743,.T.);
#14070=ORIENTED_EDGE('',*,*,#9704,.T.);
#14071=ORIENTED_EDGE('',*,*,#9744,.T.);
#14072=ORIENTED_EDGE('',*,*,#9718,.T.);
#14073=ORIENTED_EDGE('',*,*,#9745,.T.);
#14074=ORIENTED_EDGE('',*,*,#9732,.T.);
#14075=ORIENTED_EDGE('',*,*,#9789,.T.);
#14076=ORIENTED_EDGE('',*,*,#9726,.T.);
#14077=ORIENTED_EDGE('',*,*,#9790,.T.);
#14078=ORIENTED_EDGE('',*,*,#9712,.T.);
#14079=ORIENTED_EDGE('',*,*,#9791,.T.);
#14080=ORIENTED_EDGE('',*,*,#9793,.F.);
#14081=ORIENTED_EDGE('',*,*,#9794,.T.);
#14082=ORIENTED_EDGE('',*,*,#9792,.F.);
#14083=ORIENTED_EDGE('',*,*,#9795,.T.);
#14084=ORIENTED_EDGE('',*,*,#9793,.T.);
#14085=ORIENTED_EDGE('',*,*,#9795,.F.);
#14086=ORIENTED_EDGE('',*,*,#9796,.F.);
#14087=ORIENTED_EDGE('',*,*,#9775,.F.);
#14088=ORIENTED_EDGE('',*,*,#9653,.F.);
#14089=ORIENTED_EDGE('',*,*,#9776,.F.);
#14090=ORIENTED_EDGE('',*,*,#9797,.T.);
#14091=ORIENTED_EDGE('',*,*,#9796,.T.);
#14092=ORIENTED_EDGE('',*,*,#9797,.F.);
#14093=ORIENTED_EDGE('',*,*,#9670,.T.);
#14094=ORIENTED_EDGE('',*,*,#9772,.T.);
#14095=ORIENTED_EDGE('',*,*,#9782,.F.);
#14096=ORIENTED_EDGE('',*,*,#9781,.T.);
#14097=ORIENTED_EDGE('',*,*,#9794,.F.);
#14098=ORIENTED_EDGE('',*,*,#9798,.T.);
#14099=ORIENTED_EDGE('',*,*,#9783,.T.);
#14100=ORIENTED_EDGE('',*,*,#9798,.F.);
#14183=CONICAL_SURFACE('',#16742,8.75,0.785398163397448);
#15007=ADVANCED_FACE('',(#2440),#1599,.T.);
#15008=ADVANCED_FACE('',(#2441),#1600,.T.);
#15009=ADVANCED_FACE('',(#2442),#1601,.T.);
#15010=ADVANCED_FACE('',(#2443),#1602,.T.);
#15011=ADVANCED_FACE('',(#2444),#1603,.T.);
#15012=ADVANCED_FACE('',(#2445),#1604,.T.);
#15013=ADVANCED_FACE('',(#2446),#1605,.T.);
#15014=ADVANCED_FACE('',(#2447),#1606,.T.);
#15015=ADVANCED_FACE('',(#2448),#1607,.T.);
#15016=ADVANCED_FACE('',(#2449),#1608,.T.);
#15017=ADVANCED_FACE('',(#2450),#1609,.T.);
#15018=ADVANCED_FACE('',(#2451),#1610,.T.);
#15019=ADVANCED_FACE('',(#2452),#1611,.T.);
#15020=ADVANCED_FACE('',(#2453),#1612,.T.);
#15021=ADVANCED_FACE('',(#2454),#966,.T.);
#15022=ADVANCED_FACE('',(#2455),#967,.T.);
#15023=ADVANCED_FACE('',(#2456),#968,.T.);
#15024=ADVANCED_FACE('',(#2457),#969,.T.);
#15025=ADVANCED_FACE('',(#2458),#970,.T.);
#15026=ADVANCED_FACE('',(#2459),#971,.T.);
#15027=ADVANCED_FACE('',(#2460),#972,.T.);
#15028=ADVANCED_FACE('',(#2461),#973,.T.);
#15029=ADVANCED_FACE('',(#2462),#974,.T.);
#15030=ADVANCED_FACE('',(#2463),#975,.T.);
#15031=ADVANCED_FACE('',(#2464),#976,.T.);
#15032=ADVANCED_FACE('',(#2465),#977,.T.);
#15033=ADVANCED_FACE('',(#2466),#978,.T.);
#15034=ADVANCED_FACE('',(#2467),#979,.T.);
#15035=ADVANCED_FACE('',(#2468),#980,.T.);
#15036=ADVANCED_FACE('',(#2469),#981,.T.);
#15037=ADVANCED_FACE('',(#2470),#982,.T.);
#15038=ADVANCED_FACE('',(#2471),#983,.T.);
#15039=ADVANCED_FACE('',(#2472),#984,.T.);
#15040=ADVANCED_FACE('',(#2473),#985,.T.);
#15041=ADVANCED_FACE('',(#2474),#986,.T.);
#15042=ADVANCED_FACE('',(#2475,#554),#987,.T.);
#15043=ADVANCED_FACE('',(#2476),#988,.T.);
#15044=ADVANCED_FACE('',(#2477),#989,.T.);
#15045=ADVANCED_FACE('',(#2478),#990,.T.);
#15046=ADVANCED_FACE('',(#2479),#991,.T.);
#15047=ADVANCED_FACE('',(#2480),#992,.T.);
#15048=ADVANCED_FACE('',(#2481),#993,.T.);
#15049=ADVANCED_FACE('',(#2482),#994,.F.);
#15050=ADVANCED_FACE('',(#2483),#995,.F.);
#15051=ADVANCED_FACE('',(#2484),#996,.F.);
#15052=ADVANCED_FACE('',(#2485),#254,.F.);
#15053=ADVANCED_FACE('',(#2486),#997,.T.);
#15054=ADVANCED_FACE('',(#2487),#1613,.T.);
#15055=ADVANCED_FACE('',(#2488),#255,.F.);
#15056=ADVANCED_FACE('',(#2489,#555),#998,.T.);
#15057=ADVANCED_FACE('',(#2490),#999,.F.);
#15058=ADVANCED_FACE('',(#2491),#1000,.F.);
#15059=ADVANCED_FACE('',(#2492),#1001,.F.);
#15060=ADVANCED_FACE('',(#2493),#1002,.F.);
#15061=ADVANCED_FACE('',(#2494),#1003,.T.);
#15062=ADVANCED_FACE('',(#2495),#1004,.T.);
#15063=ADVANCED_FACE('',(#2496),#1005,.T.);
#15064=ADVANCED_FACE('',(#2497,#556),#1006,.T.);
#15065=ADVANCED_FACE('',(#2498,#557),#1007,.T.);
#15066=ADVANCED_FACE('',(#2499),#1614,.T.);
#15067=ADVANCED_FACE('',(#2500),#1008,.T.);
#15068=ADVANCED_FACE('',(#2501),#14183,.T.);
#15069=ADVANCED_FACE('',(#2502),#1615,.T.);
#15070=ADVANCED_FACE('',(#2503),#1616,.T.);
#15085=CLOSED_SHELL('',(#15007,#15008,#15009,#15010,#15011,#15012,#15013,
#15014,#15015,#15016,#15017,#15018,#15019,#15020,#15021,#15022,#15023,#15024,
#15025,#15026,#15027,#15028,#15029,#15030,#15031,#15032,#15033,#15034,#15035,
#15036,#15037,#15038,#15039,#15040,#15041,#15042,#15043,#15044,#15045,#15046,
#15047,#15048,#15049,#15050,#15051,#15052,#15053,#15054,#15055,#15056,#15057,
#15058,#15059,#15060,#15061,#15062,#15063,#15064,#15065,#15066,#15067,#15068,
#15069,#15070));
#16670=AXIS2_PLACEMENT_3D('',#36158,#20579,#20580);
#16671=AXIS2_PLACEMENT_3D('',#36159,#20581,#20582);
#16672=AXIS2_PLACEMENT_3D('',#36181,#20584,#20585);
#16673=AXIS2_PLACEMENT_3D('',#36192,#20586,#20587);
#16674=AXIS2_PLACEMENT_3D('',#36282,#20589,#20590);
#16675=AXIS2_PLACEMENT_3D('',#36366,#20592,#20593);
#16676=AXIS2_PLACEMENT_3D('',#36456,#20595,#20596);
#16677=AXIS2_PLACEMENT_3D('',#36546,#20598,#20599);
#16678=AXIS2_PLACEMENT_3D('',#36636,#20601,#20602);
#16679=AXIS2_PLACEMENT_3D('',#36720,#20604,#20605);
#16680=AXIS2_PLACEMENT_3D('',#36730,#20607,#20608);
#16681=AXIS2_PLACEMENT_3D('',#36731,#20609,#20610);
#16682=AXIS2_PLACEMENT_3D('',#36752,#20612,#20613);
#16683=AXIS2_PLACEMENT_3D('',#36768,#20614,#20615);
#16684=AXIS2_PLACEMENT_3D('',#36805,#20617,#20618);
#16685=AXIS2_PLACEMENT_3D('',#36843,#20620,#20621);
#16686=AXIS2_PLACEMENT_3D('',#36881,#20623,#20624);
#16687=AXIS2_PLACEMENT_3D('',#36918,#20626,#20627);
#16688=AXIS2_PLACEMENT_3D('',#36955,#20629,#20630);
#16689=AXIS2_PLACEMENT_3D('',#36962,#20634,#20635);
#16690=AXIS2_PLACEMENT_3D('',#36968,#20639,#20640);
#16691=AXIS2_PLACEMENT_3D('',#36975,#20644,#20645);
#16692=AXIS2_PLACEMENT_3D('',#36981,#20649,#20650);
#16693=AXIS2_PLACEMENT_3D('',#36984,#20653,#20654);
#16694=AXIS2_PLACEMENT_3D('',#36991,#20658,#20659);
#16695=AXIS2_PLACEMENT_3D('',#36997,#20663,#20664);
#16696=AXIS2_PLACEMENT_3D('',#37004,#20668,#20669);
#16697=AXIS2_PLACEMENT_3D('',#37010,#20673,#20674);
#16698=AXIS2_PLACEMENT_3D('',#37013,#20677,#20678);
#16699=AXIS2_PLACEMENT_3D('',#37020,#20682,#20683);
#16700=AXIS2_PLACEMENT_3D('',#37026,#20687,#20688);
#16701=AXIS2_PLACEMENT_3D('',#37033,#20692,#20693);
#16702=AXIS2_PLACEMENT_3D('',#37039,#20697,#20698);
#16703=AXIS2_PLACEMENT_3D('',#37042,#20701,#20702);
#16704=AXIS2_PLACEMENT_3D('',#37045,#20705,#20706);
#16705=AXIS2_PLACEMENT_3D('',#37048,#20709,#20710);
#16706=AXIS2_PLACEMENT_3D('',#37051,#20713,#20714);
#16707=AXIS2_PLACEMENT_3D('',#37053,#20716,#20717);
#16708=AXIS2_PLACEMENT_3D('',#37055,#20719,#20720);
#16709=AXIS2_PLACEMENT_3D('',#37057,#20722,#20723);
#16710=AXIS2_PLACEMENT_3D('',#37070,#20730,#20731);
#16711=AXIS2_PLACEMENT_3D('',#37076,#20735,#20736);
#16712=AXIS2_PLACEMENT_3D('',#37080,#20739,#20740);
#16713=AXIS2_PLACEMENT_3D('',#37086,#20744,#20745);
#16714=AXIS2_PLACEMENT_3D('',#37090,#20748,#20749);
#16715=AXIS2_PLACEMENT_3D('',#37092,#20751,#20752);
#16716=AXIS2_PLACEMENT_3D('',#37094,#20754,#20755);
#16717=AXIS2_PLACEMENT_3D('',#37100,#20759,#20760);
#16718=AXIS2_PLACEMENT_3D('',#37104,#20763,#20764);
#16719=AXIS2_PLACEMENT_3D('',#37758,#20767,#20768);
#16720=AXIS2_PLACEMENT_3D('',#37760,#20769,#20770);
#16721=AXIS2_PLACEMENT_3D('',#37761,#20771,#20772);
#16722=AXIS2_PLACEMENT_3D('',#37881,#20773,#20774);
#16723=AXIS2_PLACEMENT_3D('',#37882,#20775,#20776);
#16724=AXIS2_PLACEMENT_3D('',#38405,#20777,#20778);
#16725=AXIS2_PLACEMENT_3D('',#38406,#20779,#20780);
#16726=AXIS2_PLACEMENT_3D('',#38408,#20781,#20782);
#16727=AXIS2_PLACEMENT_3D('',#38409,#20783,#20784);
#16728=AXIS2_PLACEMENT_3D('',#38413,#20787,#20788);
#16729=AXIS2_PLACEMENT_3D('',#38417,#20791,#20792);
#16730=AXIS2_PLACEMENT_3D('',#38419,#20794,#20795);
#16731=AXIS2_PLACEMENT_3D('',#38420,#20796,#20797);
#16732=AXIS2_PLACEMENT_3D('',#38422,#20799,#20800);
#16733=AXIS2_PLACEMENT_3D('',#38424,#20802,#20803);
#16734=AXIS2_PLACEMENT_3D('',#38426,#20805,#20806);
#16735=AXIS2_PLACEMENT_3D('',#38428,#20807,#20808);
#16736=AXIS2_PLACEMENT_3D('',#38429,#20809,#20810);
#16737=AXIS2_PLACEMENT_3D('',#38431,#20811,#20812);
#16738=AXIS2_PLACEMENT_3D('',#38433,#20813,#20814);
#16739=AXIS2_PLACEMENT_3D('',#38434,#20815,#20816);
#16740=AXIS2_PLACEMENT_3D('',#38436,#20818,#20819);
#16741=AXIS2_PLACEMENT_3D('',#38438,#20820,#20821);
#16742=AXIS2_PLACEMENT_3D('',#38439,#20822,#20823);
#16743=AXIS2_PLACEMENT_3D('',#38441,#20825,#20826);
#16744=AXIS2_PLACEMENT_3D('',#38442,#20827,#20828);
#20579=DIRECTION('axis',(0.,0.,1.));
#20580=DIRECTION('refdir',(1.,0.,0.));
#20581=DIRECTION('center_axis',(1.,0.,0.));
#20582=DIRECTION('ref_axis',(0.,1.,0.));
#20583=DIRECTION('',(-1.,0.,0.));
#20584=DIRECTION('center_axis',(1.,0.,0.));
#20585=DIRECTION('ref_axis',(0.,1.,0.));
#20586=DIRECTION('center_axis',(1.,0.,0.));
#20587=DIRECTION('ref_axis',(0.,1.,0.));
#20588=DIRECTION('',(-1.,0.,0.));
#20589=DIRECTION('center_axis',(1.,0.,0.));
#20590=DIRECTION('ref_axis',(0.,1.,0.));
#20591=DIRECTION('',(-1.,0.,0.));
#20592=DIRECTION('center_axis',(1.,0.,0.));
#20593=DIRECTION('ref_axis',(0.,1.,0.));
#20594=DIRECTION('',(-1.,0.,0.));
#20595=DIRECTION('center_axis',(1.,0.,0.));
#20596=DIRECTION('ref_axis',(0.,1.,0.));
#20597=DIRECTION('',(-1.,0.,0.));
#20598=DIRECTION('center_axis',(1.,0.,0.));
#20599=DIRECTION('ref_axis',(0.,1.,0.));
#20600=DIRECTION('',(-1.,0.,0.));
#20601=DIRECTION('center_axis',(1.,0.,0.));
#20602=DIRECTION('ref_axis',(0.,1.,0.));
#20603=DIRECTION('',(-1.,0.,0.));
#20604=DIRECTION('center_axis',(1.,0.,0.));
#20605=DIRECTION('ref_axis',(0.,1.,1.99201639031977E-14));
#20606=DIRECTION('',(1.,0.,0.));
#20607=DIRECTION('center_axis',(1.,0.,0.));
#20608=DIRECTION('ref_axis',(0.,1.,1.99201639031977E-14));
#20609=DIRECTION('center_axis',(1.,0.,0.));
#20610=DIRECTION('ref_axis',(0.,1.,1.99201639031977E-14));
#20611=DIRECTION('',(1.,0.,0.));
#20612=DIRECTION('center_axis',(1.,0.,0.));
#20613=DIRECTION('ref_axis',(0.,1.,1.99201639031977E-14));
#20614=DIRECTION('center_axis',(1.,0.,0.));
#20615=DIRECTION('ref_axis',(0.,1.,1.99201639031977E-14));
#20616=DIRECTION('',(1.,0.,0.));
#20617=DIRECTION('center_axis',(1.,0.,0.));
#20618=DIRECTION('ref_axis',(0.,1.,1.99201639031977E-14));
#20619=DIRECTION('',(1.,0.,0.));
#20620=DIRECTION('center_axis',(1.,0.,0.));
#20621=DIRECTION('ref_axis',(0.,1.,1.99201639031977E-14));
#20622=DIRECTION('',(1.,0.,0.));
#20623=DIRECTION('center_axis',(1.,0.,0.));
#20624=DIRECTION('ref_axis',(0.,1.,1.99201639031977E-14));
#20625=DIRECTION('',(1.,0.,0.));
#20626=DIRECTION('center_axis',(1.,0.,0.));
#20627=DIRECTION('ref_axis',(0.,1.,1.99201639031977E-14));
#20628=DIRECTION('',(1.,0.,0.));
#20629=DIRECTION('center_axis',(0.547750005235851,-0.72455327535185,0.418321028566616));
#20630=DIRECTION('ref_axis',(0.606949534647157,0.,-0.79474037420506));
#20631=DIRECTION('',(0.67749794402081,0.0907675134870617,-0.729902592366236));
#20632=DIRECTION('',(0.,0.5,0.866025403784439));
#20633=DIRECTION('',(-0.677497944020809,-0.677497944020809,-0.286344323664976));
#20634=DIRECTION('center_axis',(0.,-0.866025403784439,0.5));
#20635=DIRECTION('ref_axis',(1.,0.,0.));
#20636=DIRECTION('',(0.,0.5,0.866025403784439));
#20637=DIRECTION('',(1.,0.,0.));
#20638=DIRECTION('',(-1.,0.,0.));
#20639=DIRECTION('center_axis',(0.547750005235851,0.,0.836642057133232));
#20640=DIRECTION('ref_axis',(0.836642057133232,0.,-0.547750005235851));
#20641=DIRECTION('',(0.677497944020809,-0.586730430533747,-0.443558268701262));
#20642=DIRECTION('',(0.,1.,0.));
#20643=DIRECTION('',(-0.67749794402081,-0.586730430533748,0.44355826870126));
#20644=DIRECTION('center_axis',(0.,0.,1.));
#20645=DIRECTION('ref_axis',(1.,0.,0.));
#20646=DIRECTION('',(0.,1.,0.));
#20647=DIRECTION('',(1.,0.,0.));
#20648=DIRECTION('',(-1.,0.,0.));
#20649=DIRECTION('center_axis',(0.707106781186547,-0.353553390593274,0.612372435695795));
#20650=DIRECTION('ref_axis',(0.654653670707978,0.,-0.755928946018454));
#20651=DIRECTION('',(0.,0.866025403784439,0.5));
#20652=DIRECTION('',(0.,-0.866025403784439,-0.5));
#20653=DIRECTION('center_axis',(0.547750005235851,-0.72455327535185,-0.418321028566615));
#20654=DIRECTION('ref_axis',(-0.606949534647157,0.,-0.79474037420506));
#20655=DIRECTION('',(0.677497944020809,0.677497944020809,-0.286344323664979));
#20656=DIRECTION('',(0.,-0.499999999999999,0.866025403784439));
#20657=DIRECTION('',(-0.67749794402081,-0.0907675134870617,-0.729902592366236));
#20658=DIRECTION('center_axis',(0.,-0.866025403784439,-0.5));
#20659=DIRECTION('ref_axis',(0.,0.5,-0.866025403784439));
#20660=DIRECTION('',(0.,-0.5,0.866025403784439));
#20661=DIRECTION('',(1.,0.,0.));
#20662=DIRECTION('',(-1.,0.,0.));
#20663=DIRECTION('center_axis',(0.547750005235849,0.724553275351851,0.418321028566616));
#20664=DIRECTION('ref_axis',(0.606949534647159,0.,-0.794740374205059));
#20665=DIRECTION('',(0.677497944020811,-0.677497944020808,0.286344323664977));
#20666=DIRECTION('',(0.,0.499999999999999,-0.866025403784439));
#20667=DIRECTION('',(-0.677497944020809,0.0907675134870586,0.729902592366237));
#20668=DIRECTION('center_axis',(0.,0.866025403784439,0.5));
#20669=DIRECTION('ref_axis',(0.,-0.5,0.866025403784439));
#20670=DIRECTION('',(0.,0.5,-0.866025403784439));
#20671=DIRECTION('',(1.,0.,0.));
#20672=DIRECTION('',(-1.,0.,0.));
#20673=DIRECTION('center_axis',(0.707106781186547,0.353553390593274,0.612372435695795));
#20674=DIRECTION('ref_axis',(0.654653670707978,0.,-0.755928946018454));
#20675=DIRECTION('',(0.,0.866025403784439,-0.5));
#20676=DIRECTION('',(0.,-0.866025403784439,0.5));
#20677=DIRECTION('center_axis',(0.547750005235851,0.,-0.836642057133232));
#20678=DIRECTION('ref_axis',(-0.836642057133232,0.,-0.547750005235851));
#20679=DIRECTION('',(0.67749794402081,0.586730430533747,0.44355826870126));
#20680=DIRECTION('',(0.,-1.,0.));
#20681=DIRECTION('',(-0.67749794402081,0.586730430533747,-0.44355826870126));
#20682=DIRECTION('center_axis',(0.,0.,-1.));
#20683=DIRECTION('ref_axis',(-1.,0.,0.));
#20684=DIRECTION('',(0.,-1.,0.));
#20685=DIRECTION('',(1.,0.,0.));
#20686=DIRECTION('',(-1.,0.,0.));
#20687=DIRECTION('center_axis',(0.547750005235848,0.724553275351853,-0.418321028566616));
#20688=DIRECTION('ref_axis',(-0.60694953464716,0.,-0.794740374205058));
#20689=DIRECTION('',(0.67749794402081,-0.0907675134870617,0.729902592366236));
#20690=DIRECTION('',(0.,-0.499999999999999,-0.866025403784439));
#20691=DIRECTION('',(-0.67749794402081,0.677497944020807,0.286344323664981));
#20692=DIRECTION('center_axis',(0.,0.866025403784439,-0.499999999999999));
#20693=DIRECTION('ref_axis',(0.,0.499999999999999,0.866025403784439));
#20694=DIRECTION('',(0.,-0.499999999999999,-0.866025403784439));
#20695=DIRECTION('',(1.,0.,0.));
#20696=DIRECTION('',(-1.,0.,0.));
#20697=DIRECTION('center_axis',(0.707106781186546,0.707106781186549,-2.47225446456458E-16));
#20698=DIRECTION('ref_axis',(-3.49629579342468E-16,0.,-1.));
#20699=DIRECTION('',(0.,-3.49629579342466E-16,-1.));
#20700=DIRECTION('',(0.,3.49629579342466E-16,1.));
#20701=DIRECTION('center_axis',(0.707106781186547,0.353553390593274,-0.612372435695795));
#20702=DIRECTION('ref_axis',(-0.654653670707978,0.,-0.755928946018454));
#20703=DIRECTION('',(0.,-0.866025403784439,-0.5));
#20704=DIRECTION('',(0.,0.866025403784439,0.5));
#20705=DIRECTION('center_axis',(0.707106781186547,-0.353553390593274,-0.612372435695795));
#20706=DIRECTION('ref_axis',(-0.654653670707978,0.,-0.755928946018454));
#20707=DIRECTION('',(0.,-0.866025403784439,0.5));
#20708=DIRECTION('',(0.,0.866025403784439,-0.5));
#20709=DIRECTION('center_axis',(0.707106781186548,-0.707106781186548,0.));
#20710=DIRECTION('ref_axis',(0.,0.,-1.));
#20711=DIRECTION('',(0.,0.,1.));
#20712=DIRECTION('',(0.,0.,-1.));
#20713=DIRECTION('center_axis',(0.,-0.5,0.866025403784439));
#20714=DIRECTION('ref_axis',(0.,-0.866025403784439,-0.5));
#20715=DIRECTION('',(0.,0.866025403784439,0.5));
#20716=DIRECTION('center_axis',(0.,0.5,0.866025403784439));
#20717=DIRECTION('ref_axis',(0.,-0.866025403784439,0.5));
#20718=DIRECTION('',(0.,0.866025403784439,-0.5));
#20719=DIRECTION('center_axis',(0.,1.,-3.49629579342466E-16));
#20720=DIRECTION('ref_axis',(0.,3.49629579342466E-16,1.));
#20721=DIRECTION('',(0.,-3.49629579342466E-16,-1.));
#20722=DIRECTION('center_axis',(1.,0.,0.));
#20723=DIRECTION('ref_axis',(0.,0.,-1.));
#20724=DIRECTION('',(0.,-0.866025403784439,0.5));
#20725=DIRECTION('',(0.,3.60555503696918E-16,1.));
#20726=DIRECTION('',(0.,0.866025403784439,0.5));
#20727=DIRECTION('',(0.,0.866025403784439,-0.5));
#20728=DIRECTION('',(0.,1.20185167898973E-16,-1.));
#20729=DIRECTION('',(0.,-0.866025403784439,-0.5));
#20730=DIRECTION('center_axis',(0.707106781186548,0.353553390593274,0.612372435695794));
#20731=DIRECTION('ref_axis',(0.654653670707977,0.,-0.755928946018455));
#20732=DIRECTION('',(-0.654653670707977,3.42727999801544E-16,0.755928946018454));
#20733=DIRECTION('',(0.,-0.866025403784439,0.5));
#20734=DIRECTION('',(-0.654653670707977,0.654653670707977,0.377964473009228));
#20735=DIRECTION('center_axis',(0.707106781186548,-0.353553390593274,0.612372435695795));
#20736=DIRECTION('ref_axis',(0.654653670707977,0.,-0.755928946018454));
#20737=DIRECTION('',(-0.654653670707977,-0.654653670707976,0.377964473009229));
#20738=DIRECTION('',(0.,-0.866025403784439,-0.5));
#20739=DIRECTION('center_axis',(0.707106781186547,-0.353553390593274,-0.612372435695795));
#20740=DIRECTION('ref_axis',(-0.654653670707978,0.,-0.755928946018454));
#20741=DIRECTION('',(-0.654653670707977,3.70298385649733E-16,-0.755928946018454));
#20742=DIRECTION('',(0.,0.866025403784439,-0.5));
#20743=DIRECTION('',(0.654653670707978,0.654653670707977,0.377964473009227));
#20744=DIRECTION('center_axis',(0.707106781186548,0.353553390593274,-0.612372435695794));
#20745=DIRECTION('ref_axis',(-0.654653670707977,0.,-0.755928946018455));
#20746=DIRECTION('',(0.,0.866025403784439,0.5));
#20747=DIRECTION('',(-0.654653670707977,0.654653670707977,-0.377964473009228));
#20748=DIRECTION('center_axis',(0.707106781186547,-0.707106781186548,2.54951241658222E-16));
#20749=DIRECTION('ref_axis',(3.60555503696919E-16,0.,-1.));
#20750=DIRECTION('',(0.,-3.60555503696918E-16,-1.));
#20751=DIRECTION('center_axis',(0.707106781186548,0.707106781186548,8.49837472194074E-17));
#20752=DIRECTION('ref_axis',(1.20185167898973E-16,0.,-1.));
#20753=DIRECTION('',(0.,-1.20185167898973E-16,1.));
#20754=DIRECTION('center_axis',(0.,0.5,-0.866025403784439));
#20755=DIRECTION('ref_axis',(0.,-0.866025403784439,-0.5));
#20756=DIRECTION('',(-1.,0.,0.));
#20757=DIRECTION('',(0.,-0.866025403784439,-0.5));
#20758=DIRECTION('',(-1.,0.,0.));
#20759=DIRECTION('center_axis',(0.,1.,-3.60555503696918E-16));
#20760=DIRECTION('ref_axis',(0.,-3.60555503696918E-16,-1.));
#20761=DIRECTION('',(-1.,0.,0.));
#20762=DIRECTION('',(0.,-3.60555503696918E-16,-1.));
#20763=DIRECTION('center_axis',(0.,0.5,0.866025403784439));
#20764=DIRECTION('ref_axis',(0.,0.866025403784439,-0.5));
#20765=DIRECTION('',(-1.,0.,0.));
#20766=DIRECTION('',(0.,0.866025403784439,-0.5));
#20767=DIRECTION('center_axis',(1.,0.,0.));
#20768=DIRECTION('ref_axis',(0.,0.,-1.));
#20769=DIRECTION('center_axis',(1.,0.,0.));
#20770=DIRECTION('ref_axis',(0.,1.,0.));
#20771=DIRECTION('center_axis',(1.,0.,0.));
#20772=DIRECTION('ref_axis',(0.,1.,0.));
#20773=DIRECTION('center_axis',(-1.,0.,0.));
#20774=DIRECTION('ref_axis',(0.,1.,1.99201639031977E-14));
#20775=DIRECTION('center_axis',(1.,0.,0.));
#20776=DIRECTION('ref_axis',(0.,1.,1.99201639031977E-14));
#20777=DIRECTION('center_axis',(1.,0.,0.));
#20778=DIRECTION('ref_axis',(0.,0.,-1.));
#20779=DIRECTION('center_axis',(-1.,0.,0.));
#20780=DIRECTION('ref_axis',(0.,1.,0.));
#20781=DIRECTION('center_axis',(1.,0.,0.));
#20782=DIRECTION('ref_axis',(0.,0.,-1.));
#20783=DIRECTION('center_axis',(0.,-0.5,0.866025403784439));
#20784=DIRECTION('ref_axis',(0.,0.866025403784439,0.5));
#20785=DIRECTION('',(-1.,0.,0.));
#20786=DIRECTION('',(0.,0.866025403784439,0.5));
#20787=DIRECTION('center_axis',(0.,-1.,-1.20185167898973E-16));
#20788=DIRECTION('ref_axis',(0.,-1.20185167898973E-16,1.));
#20789=DIRECTION('',(-1.,0.,0.));
#20790=DIRECTION('',(0.,-1.20185167898973E-16,1.));
#20791=DIRECTION('center_axis',(0.,-0.5,-0.866025403784439));
#20792=DIRECTION('ref_axis',(0.,-0.866025403784439,0.5));
#20793=DIRECTION('',(0.,-0.866025403784439,0.5));
#20794=DIRECTION('center_axis',(-1.,0.,0.));
#20795=DIRECTION('ref_axis',(0.,0.,1.));
#20796=DIRECTION('center_axis',(0.,0.5,-0.866025403784439));
#20797=DIRECTION('ref_axis',(0.,0.866025403784439,0.5));
#20798=DIRECTION('',(0.,-0.866025403784439,-0.5));
#20799=DIRECTION('center_axis',(0.,-0.5,-0.866025403784439));
#20800=DIRECTION('ref_axis',(0.,0.866025403784439,-0.5));
#20801=DIRECTION('',(0.,-0.866025403784439,0.5));
#20802=DIRECTION('center_axis',(0.,-1.,0.));
#20803=DIRECTION('ref_axis',(0.,0.,-1.));
#20804=DIRECTION('',(0.,0.,1.));
#20805=DIRECTION('center_axis',(1.,0.,0.));
#20806=DIRECTION('ref_axis',(0.,0.,-1.));
#20807=DIRECTION('center_axis',(1.,0.,0.));
#20808=DIRECTION('ref_axis',(0.,0.,-1.));
#20809=DIRECTION('center_axis',(-1.,0.,0.));
#20810=DIRECTION('ref_axis',(0.,0.,1.));
#20811=DIRECTION('center_axis',(1.,0.,0.));
#20812=DIRECTION('ref_axis',(0.,0.,-1.));
#20813=DIRECTION('center_axis',(1.,0.,0.));
#20814=DIRECTION('ref_axis',(0.,0.,-1.));
#20815=DIRECTION('center_axis',(1.,0.,0.));
#20816=DIRECTION('ref_axis',(0.,1.,0.));
#20817=DIRECTION('',(-1.,0.,0.));
#20818=DIRECTION('center_axis',(-1.,0.,0.));
#20819=DIRECTION('ref_axis',(0.,0.,1.));
#20820=DIRECTION('center_axis',(1.,0.,0.));
#20821=DIRECTION('ref_axis',(0.,0.,-1.));
#20822=DIRECTION('center_axis',(1.,0.,0.));
#20823=DIRECTION('ref_axis',(0.,1.,0.));
#20824=DIRECTION('',(-0.707106781186547,0.707106781186548,8.65956056235494E-17));
#20825=DIRECTION('center_axis',(1.,0.,0.));
#20826=DIRECTION('ref_axis',(0.,1.,0.));
#20827=DIRECTION('center_axis',(1.,0.,0.));
#20828=DIRECTION('ref_axis',(0.,1.,0.));
#20829=DIRECTION('',(-1.,0.,0.));
#36158=CARTESIAN_POINT('',(0.,0.,0.));
#36159=CARTESIAN_POINT('Origin',(-6.5,0.,0.));
#36160=CARTESIAN_POINT('',(-11.0923131746348,-8.92462941051898,0.000191549954296211));
#36161=CARTESIAN_POINT('',(-11.3076868253652,-8.92481439709363,0.000136450195849817));
#36162=CARTESIAN_POINT('',(-6.5,-8.925,-1.09299726823901E-15));
#36163=CARTESIAN_POINT('',(-11.575,3.89083931480654,8.03230655290357));
#36164=CARTESIAN_POINT('Ctrl Pts',(-11.0923131746348,-8.92462941051898,
0.000191549954296211));
#36165=CARTESIAN_POINT('Ctrl Pts',(-11.1048718995935,-8.92500789246107,
0.469746294508158));
#36166=CARTESIAN_POINT('Ctrl Pts',(-11.1174306245523,-8.88857179765685,
0.939242703025031));
#36167=CARTESIAN_POINT('Ctrl Pts',(-11.1299893495111,-8.81480118765077,
1.40279733933406));
#36168=CARTESIAN_POINT('Ctrl Pts',(-11.1691356476798,-8.58485377619997,
2.8477249151872));
#36169=CARTESIAN_POINT('Ctrl Pts',(-11.2082819458485,-7.99216188082716,
4.23492186077868));
#36170=CARTESIAN_POINT('Ctrl Pts',(-11.2474282440173,-7.10700456064237,
5.39990921955463));
#36171=CARTESIAN_POINT('Ctrl Pts',(-11.286574542186,-6.22184724045757,6.56489657833059));
#36172=CARTESIAN_POINT('Ctrl Pts',(-11.3257208403548,-5.0442244954608,7.507674350291));
#36173=CARTESIAN_POINT('Ctrl Pts',(-11.3648671385235,-3.71377318840326,
8.11643476640391));
#36174=CARTESIAN_POINT('Ctrl Pts',(-11.4040134366923,-2.38332188134573,
8.72519518251681));
#36175=CARTESIAN_POINT('Ctrl Pts',(-11.443159734861,-0.90004201222745,8.99993824278221));
#36176=CARTESIAN_POINT('Ctrl Pts',(-11.4823060330297,0.560184619660341,
8.90812021137253));
#36177=CARTESIAN_POINT('Ctrl Pts',(-11.5132040220198,1.71273463091833,8.8356486711171));
#36178=CARTESIAN_POINT('Ctrl Pts',(-11.5441020110099,2.85092277360137,8.53481431262945));
#36179=CARTESIAN_POINT('Ctrl Pts',(-11.575,3.89095401968739,8.03231038431322));
#36180=CARTESIAN_POINT('',(-11.575,-3.89072460992591,8.03230272149381));
#36181=CARTESIAN_POINT('Origin',(-11.575,0.,0.));
#36182=CARTESIAN_POINT('Ctrl Pts',(-11.575,-3.89072460992591,8.03230272149381));
#36183=CARTESIAN_POINT('Ctrl Pts',(-11.5358537018313,-5.20782651162706,
7.39431870116846));
#36184=CARTESIAN_POINT('Ctrl Pts',(-11.4967074036625,-6.36443119534448,
6.42659434900291));
#36185=CARTESIAN_POINT('Ctrl Pts',(-11.4575611054938,-7.2237987510989,5.2426655805034));
#36186=CARTESIAN_POINT('Ctrl Pts',(-11.418414807325,-8.08316630685333,4.05873681200389));
#36187=CARTESIAN_POINT('Ctrl Pts',(-11.3792685091563,-8.64529673464475,
2.65860362717041));
#36188=CARTESIAN_POINT('Ctrl Pts',(-11.3401222109875,-8.84347878979323,
1.20890931115065));
#36189=CARTESIAN_POINT('Ctrl Pts',(-11.3293104157801,-8.89821458587845,
0.808519011392666));
#36190=CARTESIAN_POINT('Ctrl Pts',(-11.3184986205726,-8.92518817393498,
0.404348157749692));
#36191=CARTESIAN_POINT('Ctrl Pts',(-11.3076868253652,-8.92481439709363,
0.000136450195849817));
#36192=CARTESIAN_POINT('Origin',(-6.5,0.,0.));
#36193=CARTESIAN_POINT('',(-9.59231317463479,-8.92556073748128,0.000127033491416559));
#36194=CARTESIAN_POINT('',(-9.80768682536521,-8.92567539102041,7.01672918444194E-5));
#36195=CARTESIAN_POINT('',(-6.5,-8.925,-1.09299726823901E-15));
#36196=CARTESIAN_POINT('Ctrl Pts',(-9.59231317463479,-8.92556073748128,
0.000127033491416559));
#36197=CARTESIAN_POINT('Ctrl Pts',(-9.59597002339987,-8.92565700983877,
0.136810759713388));
#36198=CARTESIAN_POINT('Ctrl Pts',(-9.59962687216495,-8.92258036831299,
0.273490150281187));
#36199=CARTESIAN_POINT('Ctrl Pts',(-9.60328372093003,-8.91630184308366,
0.410022300018877));
#36200=CARTESIAN_POINT('Ctrl Pts',(-9.64243001909878,-8.8490906904009,1.87158896208352));
#36201=CARTESIAN_POINT('Ctrl Pts',(-9.68157631726752,-8.41495821228372,
3.31628249397104));
#36202=CARTESIAN_POINT('Ctrl Pts',(-9.72072261543627,-7.66538193801836,
4.57279745790092));
#36203=CARTESIAN_POINT('Ctrl Pts',(-9.75986891360501,-6.91580566375299,
5.8293124218308));
#36204=CARTESIAN_POINT('Ctrl Pts',(-9.79901521177375,-5.85078559333945,
6.89764881780305));
#36205=CARTESIAN_POINT('Ctrl Pts',(-9.83816150994249,-4.59660714585951,
7.65112799401389));
#36206=CARTESIAN_POINT('Ctrl Pts',(-9.87730780811124,-3.34242869837957,
8.40460717022472));
#36207=CARTESIAN_POINT('Ctrl Pts',(-9.91645410627998,-1.89909187383322,
8.84322912667415));
#36208=CARTESIAN_POINT('Ctrl Pts',(-9.95560040444873,-0.437741236130637,
8.91498398627114));
#36209=CARTESIAN_POINT('Ctrl Pts',(-9.99474670261747,1.02360940157195,8.98673884586812));
#36210=CARTESIAN_POINT('Ctrl Pts',(-10.0338930007862,2.50297385243078,8.69162660861266));
#36211=CARTESIAN_POINT('Ctrl Pts',(-10.073039298955,3.82493555385304,8.06464040206903));
#36212=CARTESIAN_POINT('Ctrl Pts',(-10.1121855971237,5.14689725527529,7.4376541955254));
#36213=CARTESIAN_POINT('Ctrl Pts',(-10.1513318952925,6.31145620726098,6.4787940196936));
#36214=CARTESIAN_POINT('Ctrl Pts',(-10.1904781934612,7.18052410640066,5.30175729819094));
#36215=CARTESIAN_POINT('Ctrl Pts',(-10.2296244916299,8.04959200554035,4.12472057668828));
#36216=CARTESIAN_POINT('Ctrl Pts',(-10.2687707897987,8.62316885183402,2.72950730951476));
#36217=CARTESIAN_POINT('Ctrl Pts',(-10.3079170879674,8.83324241194816,1.28155581867923));
#36218=CARTESIAN_POINT('Ctrl Pts',(-10.3470633861362,9.0433159720623,-0.166395672156314));
#36219=CARTESIAN_POINT('Ctrl Pts',(-10.3862096843049,8.8898862459969,-1.66708538665386));
#36220=CARTESIAN_POINT('Ctrl Pts',(-10.4253559824737,8.39114626135687,-3.0425681824554));
#36221=CARTESIAN_POINT('Ctrl Pts',(-10.4645022806424,7.89240627671684,-4.41805097825693));
#36222=CARTESIAN_POINT('Ctrl Pts',(-10.5036485788111,7.04835603350219,-5.66832685536245));
#36223=CARTESIAN_POINT('Ctrl Pts',(-10.5427948769799,5.95907931141562,-6.64514342149727));
#36224=CARTESIAN_POINT('Ctrl Pts',(-10.5819411751486,4.86980258932905,-7.62195998763208));
#36225=CARTESIAN_POINT('Ctrl Pts',(-10.6210874733174,3.53529938837056,-8.32531724279619));
#36226=CARTESIAN_POINT('Ctrl Pts',(-10.6602337714861,2.11380926617132,-8.6718144581943));
#36227=CARTESIAN_POINT('Ctrl Pts',(-10.6993800696549,0.692319143972085,
-9.01831167359242));
#36228=CARTESIAN_POINT('Ctrl Pts',(-10.7385263678236,-0.816157899467901,
-9.00794884922453));
#36229=CARTESIAN_POINT('Ctrl Pts',(-10.7776726659923,-2.23275327449356,
-8.64195417971889));
#36230=CARTESIAN_POINT('Ctrl Pts',(-10.8168189641611,-3.6493486495192,-8.27595951021326));
#36231=CARTESIAN_POINT('Ctrl Pts',(-10.8559652623299,-4.97406235613052,
-7.55433299556987));
#36232=CARTESIAN_POINT('Ctrl Pts',(-10.8951115604986,-6.04981560800573,
-6.56264309955188));
#36233=CARTESIAN_POINT('Ctrl Pts',(-10.9342578586673,-7.12556885988095,
-5.57095320353389));
#36234=CARTESIAN_POINT('Ctrl Pts',(-10.9734041568361,-7.95236165702006,
-4.30919992614128));
#36235=CARTESIAN_POINT('Ctrl Pts',(-11.0125504550048,-8.43215659182522,
-2.92699418438758));
#36236=CARTESIAN_POINT('Ctrl Pts',(-11.0391380282148,-8.75802604951765,
-1.98822096522559));
#36237=CARTESIAN_POINT('Ctrl Pts',(-11.0657256014248,-8.92382814157034,
-0.9938839782484));
#36238=CARTESIAN_POINT('Ctrl Pts',(-11.0923131746348,-8.92462941051898,
0.000191549954296211));
#36239=CARTESIAN_POINT('Ctrl Pts',(-11.3076868253652,-8.92481439709363,
0.000136450195849817));
#36240=CARTESIAN_POINT('Ctrl Pts',(-11.2793523224039,-8.92383483904475,
-1.05918234052572));
#36241=CARTESIAN_POINT('Ctrl Pts',(-11.2510178194426,-8.73503129140792,
-2.11878171932437));
#36242=CARTESIAN_POINT('Ctrl Pts',(-11.2226833164813,-8.36587060142851,
-3.11135005349452));
#36243=CARTESIAN_POINT('Ctrl Pts',(-11.1835370183126,-7.85584667540975,
-4.48265965491388));
#36244=CARTESIAN_POINT('Ctrl Pts',(-11.1443907201438,-7.00156514086668,
-5.72602341054655));
#36245=CARTESIAN_POINT('Ctrl Pts',(-11.1052444219751,-5.90430480280725,
-6.69387629700437));
#36246=CARTESIAN_POINT('Ctrl Pts',(-11.0660981238063,-4.80704446474782,
-7.6617291834622));
#36247=CARTESIAN_POINT('Ctrl Pts',(-11.0269518256376,-3.46680532317205,
-8.35407120074516));
#36248=CARTESIAN_POINT('Ctrl Pts',(-10.9878055274688,-2.04251633415933,
-8.68887438049484));
#36249=CARTESIAN_POINT('Ctrl Pts',(-10.9486592293001,-0.618227345146618,
-9.02367756024451));
#36250=CARTESIAN_POINT('Ctrl Pts',(-10.9095129311313,0.890111491303043,
-9.00094190246089));
#36251=CARTESIAN_POINT('Ctrl Pts',(-10.8703666329626,2.30365266680068,-8.62332933535961));
#36252=CARTESIAN_POINT('Ctrl Pts',(-10.8312203347939,3.7171938422983,-8.24571676825833));
#36253=CARTESIAN_POINT('Ctrl Pts',(-10.7920740366251,5.03593735684391,-7.51322729183939));
#36254=CARTESIAN_POINT('Ctrl Pts',(-10.7529277384564,6.10350998281732,-6.51273355601827));
#36255=CARTESIAN_POINT('Ctrl Pts',(-10.7137814402876,7.17108260879073,-5.51223982019713));
#36256=CARTESIAN_POINT('Ctrl Pts',(-10.6746351421189,7.98748434619194,-4.24374182497381));
#36257=CARTESIAN_POINT('Ctrl Pts',(-10.6354888439501,8.45591106563375,-2.85764374611716));
#36258=CARTESIAN_POINT('Ctrl Pts',(-10.5963425457814,8.92433778507555,-1.47154566726051));
#36259=CARTESIAN_POINT('Ctrl Pts',(-10.5571962476126,9.04478948655795,0.0321524952294505));
#36260=CARTESIAN_POINT('Ctrl Pts',(-10.5180499494439,8.80298291682458,1.47514434110348));
#36261=CARTESIAN_POINT('Ctrl Pts',(-10.4789036512752,8.56117634709121,2.91813618697751));
#36262=CARTESIAN_POINT('Ctrl Pts',(-10.4397573531064,7.95711150614207,4.30042171623559));
#36263=CARTESIAN_POINT('Ctrl Pts',(-10.4006110549377,7.06241607297462,5.4580978224497));
#36264=CARTESIAN_POINT('Ctrl Pts',(-10.3614647567689,6.16772063980717,6.61577392866381));
#36265=CARTESIAN_POINT('Ctrl Pts',(-10.3223184586002,4.98239461442141,7.54884061183394));
#36266=CARTESIAN_POINT('Ctrl Pts',(-10.2831721604314,3.64698861005168,8.14665775885583));
#36267=CARTESIAN_POINT('Ctrl Pts',(-10.2440258622627,2.31158260568195,8.74447490587773));
#36268=CARTESIAN_POINT('Ctrl Pts',(-10.2048795640939,0.826096622328247,
9.00704251675139));
#36269=CARTESIAN_POINT('Ctrl Pts',(-10.1657332659252,-0.63332683218053,
8.90322705714482));
#36270=CARTESIAN_POINT('Ctrl Pts',(-10.1265869677565,-2.09275028668929,
8.79941159753826));
#36271=CARTESIAN_POINT('Ctrl Pts',(-10.0874406695877,-3.52611121235313,
8.32921306745147));
#36272=CARTESIAN_POINT('Ctrl Pts',(-10.048294371419,-4.76344798469274,7.54838525418809));
#36273=CARTESIAN_POINT('Ctrl Pts',(-10.0091480732502,-6.00078475703235,
6.76755744092469));
#36274=CARTESIAN_POINT('Ctrl Pts',(-9.97000177508148,-7.04209737604773,
5.67610034448468));
#36275=CARTESIAN_POINT('Ctrl Pts',(-9.93085547691274,-7.76391152766168,
4.40343432141847));
#36276=CARTESIAN_POINT('Ctrl Pts',(-9.89170917874399,-8.48572567927564,
3.13076829835225));
#36277=CARTESIAN_POINT('Ctrl Pts',(-9.85256288057525,-8.88804136348817,
1.67689334865984));
#36278=CARTESIAN_POINT('Ctrl Pts',(-9.81341658240651,-8.92315375777354,
0.214203524598343));
#36279=CARTESIAN_POINT('Ctrl Pts',(-9.81150666339274,-8.9248668655922,0.142839966946539));
#36280=CARTESIAN_POINT('Ctrl Pts',(-9.80959674437898,-8.92570588559066,
0.0714554264371891));
#36281=CARTESIAN_POINT('Ctrl Pts',(-9.80768682536521,-8.92567539102041,
7.01672918444194E-5));
#36282=CARTESIAN_POINT('Origin',(-6.5,0.,0.));
#36283=CARTESIAN_POINT('',(-8.09231317463479,-8.92541637255294,-0.000168493799423963));
#36284=CARTESIAN_POINT('',(-8.3076868253652,-8.92523072360173,-0.000199919135830939));
#36285=CARTESIAN_POINT('',(-6.5,-8.925,-1.09299726823901E-15));
#36286=CARTESIAN_POINT('Ctrl Pts',(-8.09231317463479,-8.92541637255294,
-0.000168493799423963));
#36287=CARTESIAN_POINT('Ctrl Pts',(-8.12621444537494,-8.9243130827288,1.26703437378749));
#36288=CARTESIAN_POINT('Ctrl Pts',(-8.16011571611509,-8.6515517834059,2.53469718746515));
#36289=CARTESIAN_POINT('Ctrl Pts',(-8.19401698685524,-8.12793759489029,
3.68852101759875));
#36290=CARTESIAN_POINT('Ctrl Pts',(-8.23316328502399,-7.52331255572497,
5.02085844042932));
#36291=CARTESIAN_POINT('Ctrl Pts',(-8.27230958319273,-6.58420875081621,
6.20140680939712));
#36292=CARTESIAN_POINT('Ctrl Pts',(-8.31145588136147,-5.42198099946788,
7.09018186544674));
#36293=CARTESIAN_POINT('Ctrl Pts',(-8.35060217953022,-4.25975324811955,
7.97895692149635));
#36294=CARTESIAN_POINT('Ctrl Pts',(-8.38974847769897,-2.87440155033164,
8.57595866462779));
#36295=CARTESIAN_POINT('Ctrl Pts',(-8.42889477586771,-1.43019484759195,
8.81039724085228));
#36296=CARTESIAN_POINT('Ctrl Pts',(-8.46804107403645,0.0140118551477458,
9.04483581707676));
#36297=CARTESIAN_POINT('Ctrl Pts',(-8.5071873722052,1.51707356283922,8.91671122639429));
#36298=CARTESIAN_POINT('Ctrl Pts',(-8.54633367037394,2.90076379616502,8.44121592204365));
#36299=CARTESIAN_POINT('Ctrl Pts',(-8.58547996854268,4.28445402949081,7.96572061769302));
#36300=CARTESIAN_POINT('Ctrl Pts',(-8.62462626671143,5.54877278845092,7.1428545996742));
#36301=CARTESIAN_POINT('Ctrl Pts',(-8.66377256488017,6.54380268775666,6.07018971922621));
#36302=CARTESIAN_POINT('Ctrl Pts',(-8.70291886304892,7.53883258706239,4.99752483877823));
#36303=CARTESIAN_POINT('Ctrl Pts',(-8.74206516121767,8.26457362671375,3.67506109590106));
#36304=CARTESIAN_POINT('Ctrl Pts',(-8.78121145938641,8.63497061035309,2.25961045360547));
#36305=CARTESIAN_POINT('Ctrl Pts',(-8.82035775755515,9.00536759399241,0.844159811309901));
#36306=CARTESIAN_POINT('Ctrl Pts',(-8.85950405572389,9.02042052161972,-0.664277730404096));
#36307=CARTESIAN_POINT('Ctrl Pts',(-8.89865035389264,8.67834448295411,-2.08683824933599));
#36308=CARTESIAN_POINT('Ctrl Pts',(-8.93779665206138,8.33626844428848,-3.5093987682679));
#36309=CARTESIAN_POINT('Ctrl Pts',(-8.97694295023013,7.63706343932992,-4.84608226441771));
#36310=CARTESIAN_POINT('Ctrl Pts',(-9.01608924839887,6.66363813757495,-5.93839065867938));
#36311=CARTESIAN_POINT('Ctrl Pts',(-9.05523554656762,5.69021283581997,-7.03069905294104));
#36312=CARTESIAN_POINT('Ctrl Pts',(-9.09438184473636,4.44256723726859,-7.87863234531457));
#36313=CARTESIAN_POINT('Ctrl Pts',(-9.1335281429051,3.06864169681512,-8.38164631683088));
#36314=CARTESIAN_POINT('Ctrl Pts',(-9.17267444107385,1.69471615636164,-8.8846602883472));
#36315=CARTESIAN_POINT('Ctrl Pts',(-9.21182073924259,0.19451067400608,-9.0427549390063));
#36316=CARTESIAN_POINT('Ctrl Pts',(-9.25096703741133,-1.254086949632,-8.83718409710341));
#36317=CARTESIAN_POINT('Ctrl Pts',(-9.29011333558007,-2.70268457327008,
-8.63161325520051));
#36318=CARTESIAN_POINT('Ctrl Pts',(-9.32925963374882,-4.09967433819068,
-8.06237692073562));
#36319=CARTESIAN_POINT('Ctrl Pts',(-9.36840593191757,-5.27940731184295,
-7.19697264687959));
#36320=CARTESIAN_POINT('Ctrl Pts',(-9.40755223008631,-6.45914028549521,
-6.33156837302357));
#36321=CARTESIAN_POINT('Ctrl Pts',(-9.44669852825506,-7.42161646787914,
-5.16999615977641));
#36322=CARTESIAN_POINT('Ctrl Pts',(-9.4858448264238,-8.05270964544695,-3.84999015703196));
#36323=CARTESIAN_POINT('Ctrl Pts',(-9.52133427582746,-8.62484929701108,
-2.65329242472025));
#36324=CARTESIAN_POINT('Ctrl Pts',(-9.55682372523113,-8.92462642130377,
-1.32637851751262));
#36325=CARTESIAN_POINT('Ctrl Pts',(-9.59231317463479,-8.92556073748128,
0.000127033491416559));
#36326=CARTESIAN_POINT('Ctrl Pts',(-9.80768682536521,-8.92567539102041,
7.01672918444194E-5));
#36327=CARTESIAN_POINT('Ctrl Pts',(-9.77045044621023,-8.92508085932995,
-1.39167919823139));
#36328=CARTESIAN_POINT('Ctrl Pts',(-9.73321406705525,-8.59397842659854,
-2.78370172177061));
#36329=CARTESIAN_POINT('Ctrl Pts',(-9.69597768790028,-7.9662589505002,-4.02582594453483));
#36330=CARTESIAN_POINT('Ctrl Pts',(-9.65683138973153,-7.30634264458328,
-5.33166089117597));
#36331=CARTESIAN_POINT('Ctrl Pts',(-9.61768509156279,-6.31860092839126,
-6.47182608602769));
#36332=CARTESIAN_POINT('Ctrl Pts',(-9.57853879339405,-5.12015589463028,
-7.31112574984834));
#36333=CARTESIAN_POINT('Ctrl Pts',(-9.5393924952253,-3.92171086086932,-8.15042541366897));
#36334=CARTESIAN_POINT('Ctrl Pts',(-9.50024619705655,-2.51256250953941,
-8.68885954645852));
#36335=CARTESIAN_POINT('Ctrl Pts',(-9.46109989888781,-1.05980148376962,
-8.86258297510901));
#36336=CARTESIAN_POINT('Ctrl Pts',(-9.42195360071907,0.392959542000176,
-9.03630640375949));
#36337=CARTESIAN_POINT('Ctrl Pts',(-9.38280730255033,1.88933324220986,-8.84531912827092));
#36338=CARTESIAN_POINT('Ctrl Pts',(-9.34366100438158,3.25188617149246,-8.31226758903612));
#36339=CARTESIAN_POINT('Ctrl Pts',(-9.30451470621284,4.61443910077506,-7.77921604980131));
#36340=CARTESIAN_POINT('Ctrl Pts',(-9.26536840804409,5.84317125913057,-6.90410024682028));
#36341=CARTESIAN_POINT('Ctrl Pts',(-9.22622210987535,6.79238496498866,-5.79068757957377));
#36342=CARTESIAN_POINT('Ctrl Pts',(-9.1870758117066,7.74159867084676,-4.67727491232726));
#36343=CARTESIAN_POINT('Ctrl Pts',(-9.14792951353786,8.41129392420744,-3.32556538081528));
#36344=CARTESIAN_POINT('Ctrl Pts',(-9.10878321536912,8.7220611925906,-1.89583878699597));
#36345=CARTESIAN_POINT('Ctrl Pts',(-9.06963691720037,9.03282846097377,-0.466112193176664));
#36346=CARTESIAN_POINT('Ctrl Pts',(-9.03049061903162,8.98466774437942,1.04163146294997));
#36347=CARTESIAN_POINT('Ctrl Pts',(-8.99134432086288,8.5832897299041,2.44861053777968));
#36348=CARTESIAN_POINT('Ctrl Pts',(-8.95219802269413,8.18191171542877,3.85558961260938));
#36349=CARTESIAN_POINT('Ctrl Pts',(-8.9130517245254,7.42731640307249,5.16180410614216));
#36350=CARTESIAN_POINT('Ctrl Pts',(-8.87390542635665,6.40898040252579,6.21236881989604));
#36351=CARTESIAN_POINT('Ctrl Pts',(-8.83475912818791,5.39064440197909,7.26293353364993));
#36352=CARTESIAN_POINT('Ctrl Pts',(-8.79561283001917,4.10856771324197,8.05784846762492));
#36353=CARTESIAN_POINT('Ctrl Pts',(-8.75646653185042,2.71477337922437,8.50285608797865));
#36354=CARTESIAN_POINT('Ctrl Pts',(-8.71732023368168,1.32097904520678,8.94786370833239));
#36355=CARTESIAN_POINT('Ctrl Pts',(-8.67817393551293,-0.184532934091295,
9.04296401506487));
#36356=CARTESIAN_POINT('Ctrl Pts',(-8.63902763734418,-1.62324553688074,
8.77688042991189));
#36357=CARTESIAN_POINT('Ctrl Pts',(-8.59988133917544,-3.06195813967019,
8.51079684475891));
#36358=CARTESIAN_POINT('Ctrl Pts',(-8.5607350410067,-4.43387136595102,7.88352936772046));
#36359=CARTESIAN_POINT('Ctrl Pts',(-8.52158874283795,-5.57630974936861,
6.96945663110273));
#36360=CARTESIAN_POINT('Ctrl Pts',(-8.48244244466921,-6.7187481327862,6.055383894485));
#36361=CARTESIAN_POINT('Ctrl Pts',(-8.44329614650046,-7.63171167334056,
4.85450589828798));
#36362=CARTESIAN_POINT('Ctrl Pts',(-8.40414984833172,-8.20694514987818,
3.50921749977058));
#36363=CARTESIAN_POINT('Ctrl Pts',(-8.37199550734288,-8.67943563347526,
2.4042123289676));
#36364=CARTESIAN_POINT('Ctrl Pts',(-8.33984116635404,-8.92406640251423,
1.20177635007904));
#36365=CARTESIAN_POINT('Ctrl Pts',(-8.3076868253652,-8.92523072360173,-0.000199919135830939));
#36366=CARTESIAN_POINT('Origin',(-6.5,0.,0.));
#36367=CARTESIAN_POINT('',(-6.59231317463479,-8.9244947065883,-0.000159621216041517));
#36368=CARTESIAN_POINT('',(-6.8076868253652,-8.92438047038815,-0.000115204162070208));
#36369=CARTESIAN_POINT('',(-6.5,-8.925,-1.09299726823901E-15));
#36370=CARTESIAN_POINT('Ctrl Pts',(-6.59231317463479,-8.9244947065883,-0.000159621216041517));
#36371=CARTESIAN_POINT('Ctrl Pts',(-6.61731256918127,-8.92387683722319,
0.934576087013297));
#36372=CARTESIAN_POINT('Ctrl Pts',(-6.64231196372775,-8.77761699705046,
1.86950071462885));
#36373=CARTESIAN_POINT('Ctrl Pts',(-6.66731135827423,-8.48888937989245,
2.75813595380074));
#36374=CARTESIAN_POINT('Ctrl Pts',(-6.70645765644297,-8.0367737348593,4.14964085489761));
#36375=CARTESIAN_POINT('Ctrl Pts',(-6.74560395461171,-7.23532553046888,
5.42764366535837));
#36376=CARTESIAN_POINT('Ctrl Pts',(-6.78475025278046,-6.17957698734988,
6.44060440495416));
#36377=CARTESIAN_POINT('Ctrl Pts',(-6.8238965509492,-5.12382844423088,7.45356514454996));
#36378=CARTESIAN_POINT('Ctrl Pts',(-6.86304284911794,-3.8137795623833,8.20148381328079));
#36379=CARTESIAN_POINT('Ctrl Pts',(-6.90218914728668,-2.404770204935,8.59567548859052));
#36380=CARTESIAN_POINT('Ctrl Pts',(-6.94133544545543,-0.995760847486707,
8.98986716390025));
#36381=CARTESIAN_POINT('Ctrl Pts',(-6.98048174362418,0.512208985562305,
9.03033184578887));
#36382=CARTESIAN_POINT('Ctrl Pts',(-7.01962804179292,1.94033083086948,8.71227140936716));
#36383=CARTESIAN_POINT('Ctrl Pts',(-7.05877433996167,3.36845267617666,8.39421097294545));
#36384=CARTESIAN_POINT('Ctrl Pts',(-7.09792063813041,4.71672653374201,7.7176254182134));
#36385=CARTESIAN_POINT('Ctrl Pts',(-7.13706693629915,5.82527999010435,6.76274129925055));
#36386=CARTESIAN_POINT('Ctrl Pts',(-7.1762132344679,6.93383344646669,5.8078571802877));
#36387=CARTESIAN_POINT('Ctrl Pts',(-7.21535953263664,7.80266650162602,4.57467449709404));
#36388=CARTESIAN_POINT('Ctrl Pts',(-7.25450583080539,8.32875673425172,3.20941865535734));
#36389=CARTESIAN_POINT('Ctrl Pts',(-7.29365212897413,8.85484696687742,1.84416281362066));
#36390=CARTESIAN_POINT('Ctrl Pts',(-7.33279842714287,9.03819437696948,0.346833813340936));
#36391=CARTESIAN_POINT('Ctrl Pts',(-7.37194472531162,8.85705843103853,-1.10502162552066));
#36392=CARTESIAN_POINT('Ctrl Pts',(-7.41109102348036,8.67592248510758,-2.55687706438227));
#36393=CARTESIAN_POINT('Ctrl Pts',(-7.4502373216491,8.13030318315361,-3.96325894182576));
#36394=CARTESIAN_POINT('Ctrl Pts',(-7.48938361981785,7.28489767416078,-5.15740464969601));
#36395=CARTESIAN_POINT('Ctrl Pts',(-7.52852991798659,6.43949216516796,-6.35155035756625));
#36396=CARTESIAN_POINT('Ctrl Pts',(-7.56767621615533,5.29430044913628,-7.33345989586326));
#36397=CARTESIAN_POINT('Ctrl Pts',(-7.60682251432408,3.98511434795003,-7.98670272875245));
#36398=CARTESIAN_POINT('Ctrl Pts',(-7.64596881249282,2.67592824676378,-8.63994556164165));
#36399=CARTESIAN_POINT('Ctrl Pts',(-7.68511511066157,1.20274776042295,-8.96452168912302));
#36400=CARTESIAN_POINT('Ctrl Pts',(-7.72426140883031,-0.259743816210902,
-8.92194429447076));
#36401=CARTESIAN_POINT('Ctrl Pts',(-7.76340770699906,-1.72223539284475,
-8.87936689981849));
#36402=CARTESIAN_POINT('Ctrl Pts',(-7.8025540051678,-3.17403805977162,-8.46963598303259));
#36403=CARTESIAN_POINT('Ctrl Pts',(-7.84170030333655,-4.44300341039844,
-7.74133564308426));
#36404=CARTESIAN_POINT('Ctrl Pts',(-7.88084660150529,-5.71196876102527,
-7.01303530313593));
#36405=CARTESIAN_POINT('Ctrl Pts',(-7.91999289967403,-6.79809679535206,
-5.96616554002517));
#36406=CARTESIAN_POINT('Ctrl Pts',(-7.95913919784278,-7.57259920438554,
-4.7248595887538));
#36407=CARTESIAN_POINT('Ctrl Pts',(-7.99828549601152,-8.34710161341902,
-3.48355363748243));
#36408=CARTESIAN_POINT('Ctrl Pts',(-8.03743179418027,-8.80997839715919,
-2.04781149805045));
#36409=CARTESIAN_POINT('Ctrl Pts',(-8.07657809234901,-8.90634365231834,
-0.587877189987794));
#36410=CARTESIAN_POINT('Ctrl Pts',(-8.08182311977761,-8.91925517729305,
-0.392267493849314));
#36411=CARTESIAN_POINT('Ctrl Pts',(-8.0870681472062,-8.92558706778834,-0.196223498611237));
#36412=CARTESIAN_POINT('Ctrl Pts',(-8.09231317463479,-8.92541637255294,
-0.000168493799423963));
#36413=CARTESIAN_POINT('Ctrl Pts',(-8.3076868253652,-8.92523072360173,-0.000199919135830939));
#36414=CARTESIAN_POINT('Ctrl Pts',(-8.3006948681853,-8.92548390506766,-0.261569499328123));
#36415=CARTESIAN_POINT('Ctrl Pts',(-8.29370291100539,-8.91422491072157,
-0.522917342403738));
#36416=CARTESIAN_POINT('Ctrl Pts',(-8.28671095382549,-8.89129327218942,
-0.783236938427221));
#36417=CARTESIAN_POINT('Ctrl Pts',(-8.24756465565675,-8.76290450544219,
-2.24070417726982));
#36418=CARTESIAN_POINT('Ctrl Pts',(-8.208418357488,-8.26862355942686,-3.66593985411726));
#36419=CARTESIAN_POINT('Ctrl Pts',(-8.16927205931926,-7.46706010555778,
-4.88994575979847));
#36420=CARTESIAN_POINT('Ctrl Pts',(-8.13012576115051,-6.6654966516887,-6.11395166547967));
#36421=CARTESIAN_POINT('Ctrl Pts',(-8.09097946298177,-5.55665068996587,
-7.13672779999466));
#36422=CARTESIAN_POINT('Ctrl Pts',(-8.05183316481303,-4.27200432179028,
-7.83699784537442));
#36423=CARTESIAN_POINT('Ctrl Pts',(-8.01268686664428,-2.9873579536147,-8.53726789075417));
#36424=CARTESIAN_POINT('Ctrl Pts',(-7.97354056847554,-1.52691117898638,
-8.91503184699869));
#36425=CARTESIAN_POINT('Ctrl Pts',(-7.93439427030679,-0.0638373849598622,
-8.92549611741949));
#36426=CARTESIAN_POINT('Ctrl Pts',(-7.89524797213805,1.39923640906668,-8.93596038784028));
#36427=CARTESIAN_POINT('Ctrl Pts',(-7.8561016739693,2.8649372224914,-8.57912497243734));
#36428=CARTESIAN_POINT('Ctrl Pts',(-7.81695537580056,4.15946866733332,-7.89730185311831));
#36429=CARTESIAN_POINT('Ctrl Pts',(-7.77780907763181,5.45400011217522,-7.21547873379928));
#36430=CARTESIAN_POINT('Ctrl Pts',(-7.73866277946307,6.5773621884343,-6.20866791056417));
#36431=CARTESIAN_POINT('Ctrl Pts',(-7.69951648129433,7.39635153737553,-4.99625260463822));
#36432=CARTESIAN_POINT('Ctrl Pts',(-7.66037018312558,8.21534088631675,-3.78383729871229));
#36433=CARTESIAN_POINT('Ctrl Pts',(-7.62122388495684,8.72995750794012,-2.3658175100955));
#36434=CARTESIAN_POINT('Ctrl Pts',(-7.5820775867881,8.87918041541532,-0.910335819517742));
#36435=CARTESIAN_POINT('Ctrl Pts',(-7.54293128861935,9.02840332289053,0.545145871060029));
#36436=CARTESIAN_POINT('Ctrl Pts',(-7.50378499045061,8.81223251621757,2.0380894635988));
#36437=CARTESIAN_POINT('Ctrl Pts',(-7.46463869228187,8.25630058360449,3.39146824059498));
#36438=CARTESIAN_POINT('Ctrl Pts',(-7.42549239411312,7.70036865099141,4.74484701759115));
#36439=CARTESIAN_POINT('Ctrl Pts',(-7.38634609594437,6.80467559243821,5.95866097904473));
#36440=CARTESIAN_POINT('Ctrl Pts',(-7.34719979777563,5.67542877092818,6.88898137752691));
#36441=CARTESIAN_POINT('Ctrl Pts',(-7.30805349960688,4.54618194941816,7.81930177600908));
#36442=CARTESIAN_POINT('Ctrl Pts',(-7.26890720143814,3.18338136495132,8.46612861151986));
#36443=CARTESIAN_POINT('Ctrl Pts',(-7.2297609032694,1.74862194669022,8.75276398866926));
#36444=CARTESIAN_POINT('Ctrl Pts',(-7.19061460510065,0.313862528429119,
9.03939936581866));
#36445=CARTESIAN_POINT('Ctrl Pts',(-7.15146830693191,-1.19285572362624,
8.96584328460668));
#36446=CARTESIAN_POINT('Ctrl Pts',(-7.11232200876316,-2.59287275313015,
8.54081770323353));
#36447=CARTESIAN_POINT('Ctrl Pts',(-7.07317571059442,-3.99288978263407,
8.11579212186038));
#36448=CARTESIAN_POINT('Ctrl Pts',(-7.03402941242568,-5.28620558958652,
7.33929704032606));
#36449=CARTESIAN_POINT('Ctrl Pts',(-6.99488311425694,-6.31946444565028,
6.30340584715549));
#36450=CARTESIAN_POINT('Ctrl Pts',(-6.95573681608819,-7.35272330171405,
5.26751465398492));
#36451=CARTESIAN_POINT('Ctrl Pts',(-6.91659051791944,-8.12592520688912,
3.97222734917811));
#36452=CARTESIAN_POINT('Ctrl Pts',(-6.8774442197507,-8.54738726309104,2.5711334326598));
#36453=CARTESIAN_POINT('Ctrl Pts',(-6.85419175495553,-8.79773102694041,
1.73889926256976));
#36454=CARTESIAN_POINT('Ctrl Pts',(-6.83093929016037,-8.92397296685791,
0.869334111825168));
#36455=CARTESIAN_POINT('Ctrl Pts',(-6.8076868253652,-8.92438047038815,-0.000115204162070208));
#36456=CARTESIAN_POINT('Origin',(-6.5,0.,0.));
#36457=CARTESIAN_POINT('',(-5.0923131746348,-8.92436978820107,0.000109438495129732));
#36458=CARTESIAN_POINT('',(-5.30768682536521,-8.92447940011954,0.000154963622128282));
#36459=CARTESIAN_POINT('',(-6.5,-8.925,-1.09299726823901E-15));
#36460=CARTESIAN_POINT('Ctrl Pts',(-5.0923131746348,-8.92436978820107,0.000109438495129732));
#36461=CARTESIAN_POINT('Ctrl Pts',(-5.1084106929876,-8.92463735146639,0.602025179022216));
#36462=CARTESIAN_POINT('Ctrl Pts',(-5.12450821134041,-8.86460350787768,
1.20388826880243));
#36463=CARTESIAN_POINT('Ctrl Pts',(-5.14060572969321,-8.74372518911622,
1.79327261198914));
#36464=CARTESIAN_POINT('Ctrl Pts',(-5.17975202786195,-8.44977064254175,
3.22655038367492));
#36465=CARTESIAN_POINT('Ctrl Pts',(-5.21889832603069,-7.79599659992567,
4.58603186904615));
#36466=CARTESIAN_POINT('Ctrl Pts',(-5.25804462419943,-6.85992472607204,
5.7105157031853));
#36467=CARTESIAN_POINT('Ctrl Pts',(-5.29719092236818,-5.92385285221839,
6.83499953732447));
#36468=CARTESIAN_POINT('Ctrl Pts',(-5.33633722053693,-4.70548314712719,
7.72448572023157));
#36469=CARTESIAN_POINT('Ctrl Pts',(-5.37548351870567,-3.34928455837054,
8.27350287307374));
#36470=CARTESIAN_POINT('Ctrl Pts',(-5.41462981687442,-1.99308596961389,
8.82252002591591));
#36471=CARTESIAN_POINT('Ctrl Pts',(-5.45377611504316,-0.499058497191769,
9.03106814869316));
#36472=CARTESIAN_POINT('Ctrl Pts',(-5.4929224132119,0.955642619659421,8.87441851769396));
#36473=CARTESIAN_POINT('Ctrl Pts',(-5.53206871138064,2.41034373651061,8.71776888669477));
#36474=CARTESIAN_POINT('Ctrl Pts',(-5.57121500954939,3.82571849779088,8.19592150191912));
#36475=CARTESIAN_POINT('Ctrl Pts',(-5.61036130771813,5.03393795853599,7.37075474244733));
#36476=CARTESIAN_POINT('Ctrl Pts',(-5.64950760588688,6.24215741928109,6.54558798297554));
#36477=CARTESIAN_POINT('Ctrl Pts',(-5.68865390405562,7.24322157949105,5.4171018488076));
#36478=CARTESIAN_POINT('Ctrl Pts',(-5.72780020222436,7.91842863209293,4.11910728704047));
#36479=CARTESIAN_POINT('Ctrl Pts',(-5.76694650039311,8.5936356846948,2.82111272527336));
#36480=CARTESIAN_POINT('Ctrl Pts',(-5.80609279856185,8.94298562968861,1.3536097359071));
#36481=CARTESIAN_POINT('Ctrl Pts',(-5.8452390967306,8.92505407948771,-0.109391598941135));
#36482=CARTESIAN_POINT('Ctrl Pts',(-5.88438539489934,8.90712252928682,-1.57239293378936));
#36483=CARTESIAN_POINT('Ctrl Pts',(-5.92353169306809,8.52190948389122,-3.03089261411952));
#36484=CARTESIAN_POINT('Ctrl Pts',(-5.96267799123683,7.81509182038236,-4.31194813079793));
#36485=CARTESIAN_POINT('Ctrl Pts',(-6.00182428940557,7.10827415687349,-5.59300364747637));
#36486=CARTESIAN_POINT('Ctrl Pts',(-6.04097058757431,6.07985187525134,-6.69661500050304));
#36487=CARTESIAN_POINT('Ctrl Pts',(-6.08011688574306,4.85177078889619,-7.49192078546702));
#36488=CARTESIAN_POINT('Ctrl Pts',(-6.11926318391181,3.62368970254106,-8.28722657043099));
#36489=CARTESIAN_POINT('Ctrl Pts',(-6.15840948208055,2.19594981145294,-8.77422678733228));
#36490=CARTESIAN_POINT('Ctrl Pts',(-6.1975557802493,0.737846263573978,-8.89517508175242));
#36491=CARTESIAN_POINT('Ctrl Pts',(-6.23670207841804,-0.720257284304982,
-9.01612337617255));
#36492=CARTESIAN_POINT('Ctrl Pts',(-6.27584837658678,-2.20872448897478,
-8.77101974811154));
#36493=CARTESIAN_POINT('Ctrl Pts',(-6.31499467475553,-3.55105942341503,
-8.18892751311638));
#36494=CARTESIAN_POINT('Ctrl Pts',(-6.35414097292427,-4.89339435785525,
-7.60683527812123));
#36495=CARTESIAN_POINT('Ctrl Pts',(-6.39328727109301,-6.08959702206593,
-6.68775443619196));
#36496=CARTESIAN_POINT('Ctrl Pts',(-6.43243356926176,-6.9978269391714,-5.54066557131056));
#36497=CARTESIAN_POINT('Ctrl Pts',(-6.4715798674305,-7.90605685627687,-4.39357670642917));
#36498=CARTESIAN_POINT('Ctrl Pts',(-6.51072616559924,-8.52631402627713,
-3.01847981859566));
#36499=CARTESIAN_POINT('Ctrl Pts',(-6.54987246376799,-8.78505106843932,
-1.57842787881243));
#36500=CARTESIAN_POINT('Ctrl Pts',(-6.56401936739026,-8.87855487774464,
-1.05801402217245));
#36501=CARTESIAN_POINT('Ctrl Pts',(-6.57816627101252,-8.92484435259045,
-0.529117070646644));
#36502=CARTESIAN_POINT('Ctrl Pts',(-6.59231317463479,-8.9244947065883,-0.000159621216041517));
#36503=CARTESIAN_POINT('Ctrl Pts',(-6.8076868253652,-8.92438047038815,-0.000115204162070208));
#36504=CARTESIAN_POINT('Ctrl Pts',(-6.79179299199162,-8.92465901261006,
-0.594412741081523));
#36505=CARTESIAN_POINT('Ctrl Pts',(-6.77589915861805,-8.86614547439013,
-1.18865615794793));
#36506=CARTESIAN_POINT('Ctrl Pts',(-6.76000532524447,-8.74828653057556,
-1.77088648217279));
#36507=CARTESIAN_POINT('Ctrl Pts',(-6.72085902707572,-8.45800153462939,
-3.20491195225729));
#36508=CARTESIAN_POINT('Ctrl Pts',(-6.68171272890698,-7.80770933550826,
-4.5660623641965));
#36509=CARTESIAN_POINT('Ctrl Pts',(-6.64256643073823,-6.87451873625329,
-5.69293845906439));
#36510=CARTESIAN_POINT('Ctrl Pts',(-6.60342013256949,-5.94132813699833,
-6.81981455393227));
#36511=CARTESIAN_POINT('Ctrl Pts',(-6.56427383440075,-4.72523913760954,
-7.71241633172884));
#36512=CARTESIAN_POINT('Ctrl Pts',(-6.52512753623201,-3.37045024955766,
-8.26490298001428));
#36513=CARTESIAN_POINT('Ctrl Pts',(-6.48598123806326,-2.01566136150579,
-8.81738962829971));
#36514=CARTESIAN_POINT('Ctrl Pts',(-6.44683493989451,-0.522172584790831,
-9.02976114707401));
#36515=CARTESIAN_POINT('Ctrl Pts',(-6.40768864172577,0.932924717530035,
-8.87683545106101));
#36516=CARTESIAN_POINT('Ctrl Pts',(-6.36854234355703,2.38802201985091,-8.72390975504801));
#36517=CARTESIAN_POINT('Ctrl Pts',(-6.32939604538828,3.80472784777769,-8.20568684424769));
#36518=CARTESIAN_POINT('Ctrl Pts',(-6.29024974721954,5.01505542428857,-7.38361532347845));
#36519=CARTESIAN_POINT('Ctrl Pts',(-6.2511034490508,6.22538300079946,-6.56154380270922));
#36520=CARTESIAN_POINT('Ctrl Pts',(-6.21195715088205,7.22933232589443,-5.43562367197108));
#36521=CARTESIAN_POINT('Ctrl Pts',(-6.17281085271331,7.90785948227508,-4.1393616129041));
#36522=CARTESIAN_POINT('Ctrl Pts',(-6.13366455454456,8.58638663865573,-2.84309955383713));
#36523=CARTESIAN_POINT('Ctrl Pts',(-6.09451825637582,8.93949162632205,-1.37649556644134));
#36524=CARTESIAN_POINT('Ctrl Pts',(-6.05537195820708,8.92530480116083,0.086546866885319));
#36525=CARTESIAN_POINT('Ctrl Pts',(-6.01622566003833,8.9111179759996,1.54958930021198));
#36526=CARTESIAN_POINT('Ctrl Pts',(-5.97707936186958,8.52963933801083,3.00907017946953));
#36527=CARTESIAN_POINT('Ctrl Pts',(-5.93793306370084,7.82610295458887,4.29193064924951));
#36528=CARTESIAN_POINT('Ctrl Pts',(-5.89878676553209,7.12256657116693,5.57479111902946));
#36529=CARTESIAN_POINT('Ctrl Pts',(-5.85964046736335,6.09697244231183,6.68103117933188));
#36530=CARTESIAN_POINT('Ctrl Pts',(-5.82049416919461,4.8709310314258,7.47947772514133));
#36531=CARTESIAN_POINT('Ctrl Pts',(-5.78134787102587,3.64488962053974,8.2779242709508));
#36532=CARTESIAN_POINT('Ctrl Pts',(-5.74220157285712,2.21840092762276,8.76857730226729));
#36533=CARTESIAN_POINT('Ctrl Pts',(-5.70305527468838,0.760611739013584,
8.89325732992511));
#36534=CARTESIAN_POINT('Ctrl Pts',(-5.66390897651963,-0.697177449595592,
9.01793735758293));
#36535=CARTESIAN_POINT('Ctrl Pts',(-5.62476267835089,-2.18626713389695,
8.77664438158209));
#36536=CARTESIAN_POINT('Ctrl Pts',(-5.58561638018215,-3.5300875759596,8.19798986702519));
#36537=CARTESIAN_POINT('Ctrl Pts',(-5.5464700820134,-4.87390801802225,7.61933535246829));
#36538=CARTESIAN_POINT('Ctrl Pts',(-5.50732378384466,-6.07245921784618,
6.70331929935531));
#36539=CARTESIAN_POINT('Ctrl Pts',(-5.46817748567591,-6.98362221948084,
5.55855888242316));
#36540=CARTESIAN_POINT('Ctrl Pts',(-5.42903118750717,-7.8947852211155,4.41379846549101));
#36541=CARTESIAN_POINT('Ctrl Pts',(-5.38988488933843,-8.51856002456089,
3.04029368473968));
#36542=CARTESIAN_POINT('Ctrl Pts',(-5.35073859116968,-8.7809821435047,1.60090872608144));
#36543=CARTESIAN_POINT('Ctrl Pts',(-5.33638800256819,-8.87718311384068,
1.07324653713474));
#36544=CARTESIAN_POINT('Ctrl Pts',(-5.3220374139667,-8.92482289482857,0.536730893015737));
#36545=CARTESIAN_POINT('Ctrl Pts',(-5.30768682536521,-8.92447940011954,
0.000154963622128282));
#36546=CARTESIAN_POINT('Origin',(-6.5,0.,0.));
#36547=CARTESIAN_POINT('',(-3.59231317463479,-8.92520804921716,0.00020252989606076));
#36548=CARTESIAN_POINT('',(-3.80768682536521,-8.9253958274169,0.000172963988443203));
#36549=CARTESIAN_POINT('',(-6.5,-8.925,-1.09299726823901E-15));
#36550=CARTESIAN_POINT('Ctrl Pts',(-3.59231317463479,-8.92520804921716,
0.00020252989606076));
#36551=CARTESIAN_POINT('Ctrl Pts',(-3.59950881679392,-8.92547024676361,
0.269188130100031));
#36552=CARTESIAN_POINT('Ctrl Pts',(-3.60670445895305,-8.9135447392344,0.538150566983954));
#36553=CARTESIAN_POINT('Ctrl Pts',(-3.61390010111218,-8.88925943030047,
0.805992336250304));
#36554=CARTESIAN_POINT('Ctrl Pts',(-3.65304639928093,-8.75714058341735,
2.26312618613775));
#36555=CARTESIAN_POINT('Ctrl Pts',(-3.69219269744967,-8.25921324989963,
3.68709204960042));
#36556=CARTESIAN_POINT('Ctrl Pts',(-3.73133899561841,-7.45451947889753,
4.90904228672834));
#36557=CARTESIAN_POINT('Ctrl Pts',(-3.77048529378716,-6.64982570789543,
6.13099252385626));
#36558=CARTESIAN_POINT('Ctrl Pts',(-3.8096315919559,-5.53836549940895,7.15092713464943));
#36559=CARTESIAN_POINT('Ctrl Pts',(-3.84877789012465,-4.25193093820849,
7.84790673640995));
#36560=CARTESIAN_POINT('Ctrl Pts',(-3.88792418829339,-2.96549637700803,
8.54488633817046));
#36561=CARTESIAN_POINT('Ctrl Pts',(-3.92707048646213,-1.5040874630936,8.91891093089831));
#36562=CARTESIAN_POINT('Ctrl Pts',(-3.96621678463088,-0.0409916710908219,
8.92563031535538));
#36563=CARTESIAN_POINT('Ctrl Pts',(-4.00536308279962,1.42210412091196,8.93234969981245));
#36564=CARTESIAN_POINT('Ctrl Pts',(-4.04450938096837,2.88688679100308,8.57176387599873));
#36565=CARTESIAN_POINT('Ctrl Pts',(-4.08365567913711,4.17966882128255,7.88662953279256));
#36566=CARTESIAN_POINT('Ctrl Pts',(-4.12280197730586,5.472450851562,7.20149518958641));
#36567=CARTESIAN_POINT('Ctrl Pts',(-4.1619482754746,6.59323224202979,6.19181232698781));
#36568=CARTESIAN_POINT('Ctrl Pts',(-4.20109457364334,7.40911564004151,4.97730472010364));
#36569=CARTESIAN_POINT('Ctrl Pts',(-4.24024087181208,8.22499903805323,3.76279711321948));
#36570=CARTESIAN_POINT('Ctrl Pts',(-4.27938716998083,8.73598444360888,2.34346476204975));
#36571=CARTESIAN_POINT('Ctrl Pts',(-4.31853346814957,8.88148144375866,0.887605885235826));
#36572=CARTESIAN_POINT('Ctrl Pts',(-4.35767976631832,9.02697844390845,-0.568252991578145));
#36573=CARTESIAN_POINT('Ctrl Pts',(-4.39682606448706,8.80698703865234,-2.06063839403631));
#36574=CARTESIAN_POINT('Ctrl Pts',(-4.43597236265581,8.24759284597125,-3.41258979236604));
#36575=CARTESIAN_POINT('Ctrl Pts',(-4.47511866082455,7.68819865329017,-4.76454119069574));
#36576=CARTESIAN_POINT('Ctrl Pts',(-4.5142649589933,6.78940167318409,-5.97605858489704));
#36577=CARTESIAN_POINT('Ctrl Pts',(-4.55341125716204,5.65777731811414,-6.90348554443819));
#36578=CARTESIAN_POINT('Ctrl Pts',(-4.59255755533079,4.52615296304418,-7.83091250397935));
#36579=CARTESIAN_POINT('Ctrl Pts',(-4.63170385349953,3.16170123301033,-8.47424902886039));
#36580=CARTESIAN_POINT('Ctrl Pts',(-4.67085015166827,1.72621284276808,-8.75721108944933));
#36581=CARTESIAN_POINT('Ctrl Pts',(-4.70999644983701,0.290724452525837,
-9.04017315003826));
#36582=CARTESIAN_POINT('Ctrl Pts',(-4.74914274800576,-1.2158005979248,-8.9627607463351));
#36583=CARTESIAN_POINT('Ctrl Pts',(-4.7882890461745,-2.61472516122752,-8.53415310238505));
#36584=CARTESIAN_POINT('Ctrl Pts',(-4.82743534434325,-4.01364972453022,
-8.10554545843501));
#36585=CARTESIAN_POINT('Ctrl Pts',(-4.86658164251199,-5.30497380068501,
-7.3257425742381));
#36586=CARTESIAN_POINT('Ctrl Pts',(-4.90572794068074,-6.33557783208182,
-6.28721006308237));
#36587=CARTESIAN_POINT('Ctrl Pts',(-4.94487423884948,-7.36618186347866,
-5.24867755192661));
#36588=CARTESIAN_POINT('Ctrl Pts',(-4.98402053701822,-8.13606585011751,
-3.95141541381203));
#36589=CARTESIAN_POINT('Ctrl Pts',(-5.02316683518697,-8.55394031817052,
-2.54924731575455));
#36590=CARTESIAN_POINT('Ctrl Pts',(-5.04621561500291,-8.79997882130919,
-1.72367081762046));
#36591=CARTESIAN_POINT('Ctrl Pts',(-5.06926439481886,-8.92398668524979,
-0.861726719544906));
#36592=CARTESIAN_POINT('Ctrl Pts',(-5.0923131746348,-8.92436978820107,0.000109438495129732));
#36593=CARTESIAN_POINT('Ctrl Pts',(-5.30768682536521,-8.92447940011954,
0.000154963622128282));
#36594=CARTESIAN_POINT('Ctrl Pts',(-5.28289111579795,-8.92388589170818,
-0.926969440504354));
#36595=CARTESIAN_POINT('Ctrl Pts',(-5.2580954062307,-8.78003944268694,-1.85427382489975));
#36596=CARTESIAN_POINT('Ctrl Pts',(-5.23329969666344,-8.49592120033681,
-2.73639893134377));
#36597=CARTESIAN_POINT('Ctrl Pts',(-5.1941533984947,-8.04736870378287,-4.12905649354552));
#36598=CARTESIAN_POINT('Ctrl Pts',(-5.15500710032596,-7.24919427623276,
-5.40910648138388));
#36599=CARTESIAN_POINT('Ctrl Pts',(-5.11586080215721,-6.19604194818467,
-6.42476616929583));
#36600=CARTESIAN_POINT('Ctrl Pts',(-5.07671450398847,-5.14288962013658,
-7.44042585720777));
#36601=CARTESIAN_POINT('Ctrl Pts',(-5.03756820581973,-3.83475939159051,
-8.19169524519331));
#36602=CARTESIAN_POINT('Ctrl Pts',(-4.99842190765098,-2.42676362016271,
-8.58949209707109));
#36603=CARTESIAN_POINT('Ctrl Pts',(-4.95927560948224,-1.0187678487349,-8.98728894894888));
#36604=CARTESIAN_POINT('Ctrl Pts',(-4.92012931131349,0.489093465574642,
-9.0316132647189));
#36605=CARTESIAN_POINT('Ctrl Pts',(-4.88098301314475,1.91802472710077,-8.71720926099757));
#36606=CARTESIAN_POINT('Ctrl Pts',(-4.84183671497601,3.34695598862691,-8.40280525727623));
#36607=CARTESIAN_POINT('Ctrl Pts',(-4.80269041680727,4.69695719736963,-7.72967293406355));
#36608=CARTESIAN_POINT('Ctrl Pts',(-4.76354411863852,5.80795111812432,-6.77762937635807));
#36609=CARTESIAN_POINT('Ctrl Pts',(-4.72439782046978,6.91894503887903,-5.82558581865258));
#36610=CARTESIAN_POINT('Ctrl Pts',(-4.68525152230103,7.7909316716457,-4.59463102645427));
#36611=CARTESIAN_POINT('Ctrl Pts',(-4.64610522413228,8.32051465766307,-3.230726231887));
#36612=CARTESIAN_POINT('Ctrl Pts',(-4.60695892596354,8.85009764368042,-1.86682143731975));
#36613=CARTESIAN_POINT('Ctrl Pts',(-4.5678126277948,9.03727698294849,-0.369966640383566));
#36614=CARTESIAN_POINT('Ctrl Pts',(-4.52866632962606,8.85985776858471,1.08234766791798));
#36615=CARTESIAN_POINT('Ctrl Pts',(-4.48952003145731,8.68243855422092,2.53466197621952));
#36616=CARTESIAN_POINT('Ctrl Pts',(-4.45037373328856,8.14042078622527,3.9424357958864));
#36617=CARTESIAN_POINT('Ctrl Pts',(-4.41122743511982,7.29807455944982,5.13874146834563));
#36618=CARTESIAN_POINT('Ctrl Pts',(-4.37208113695108,6.45572833267433,6.33504714080488));
#36619=CARTESIAN_POINT('Ctrl Pts',(-4.33293483878233,5.31305364711901,7.31988466605648));
#36620=CARTESIAN_POINT('Ctrl Pts',(-4.29378854061359,4.005543866204,7.97647632038817));
#36621=CARTESIAN_POINT('Ctrl Pts',(-4.25464224244485,2.69803408528902,8.63306797471983));
#36622=CARTESIAN_POINT('Ctrl Pts',(-4.2154959442761,1.22568920901436,8.96141375813161));
#36623=CARTESIAN_POINT('Ctrl Pts',(-4.17634964610736,-0.236906550731843,
8.92257986459216));
#36624=CARTESIAN_POINT('Ctrl Pts',(-4.13720334793861,-1.69950231047808,
8.88374597105271));
#36625=CARTESIAN_POINT('Ctrl Pts',(-4.09805704976987,-3.15234895369587,
8.47773240056201));
#36626=CARTESIAN_POINT('Ctrl Pts',(-4.05891075160112,-4.42317428367459,
7.75268246544155));
#36627=CARTESIAN_POINT('Ctrl Pts',(-4.01976445343238,-5.69399961365327,
7.02763253032112));
#36628=CARTESIAN_POINT('Ctrl Pts',(-3.98061815526363,-6.7828036303929,5.98354623057094));
#36629=CARTESIAN_POINT('Ctrl Pts',(-3.94147185709489,-7.56048071857314,
4.74422675027843));
#36630=CARTESIAN_POINT('Ctrl Pts',(-3.90232555892615,-8.33815780675341,
3.50490726998588));
#36631=CARTESIAN_POINT('Ctrl Pts',(-3.8631792607574,-8.80470796637427,2.07035460915098));
#36632=CARTESIAN_POINT('Ctrl Pts',(-3.82403296258866,-8.90480972139819,
0.610671744158159));
#36633=CARTESIAN_POINT('Ctrl Pts',(-3.81858425018084,-8.91874272911943,
0.407500754562134));
#36634=CARTESIAN_POINT('Ctrl Pts',(-3.81313553777302,-8.92557637671001,
0.203842906878487));
#36635=CARTESIAN_POINT('Ctrl Pts',(-3.80768682536521,-8.9253958274169,0.000172963988443203));
#36636=CARTESIAN_POINT('Origin',(-6.5,0.,0.));
#36637=CARTESIAN_POINT('',(-2.09231317463479,-8.92567592894044,-6.35753767513903E-5));
#36638=CARTESIAN_POINT('',(-2.3076868253652,-8.92557695889132,-0.000120900814251108));
#36639=CARTESIAN_POINT('',(-6.5,-8.925,-1.09299726823901E-15));
#36640=CARTESIAN_POINT('Ctrl Pts',(-2.09231317463479,-8.92567592894044,
-6.35753767513903E-5));
#36641=CARTESIAN_POINT('Ctrl Pts',(-2.12975323876899,-8.92512744453285,
1.39929403128198));
#36642=CARTESIAN_POINT('Ctrl Pts',(-2.16719330290319,-8.59027658419489,
2.79890392264426));
#36643=CARTESIAN_POINT('Ctrl Pts',(-2.20463336703739,-7.95593258617703,
4.04620331871739));
#36644=CARTESIAN_POINT('Ctrl Pts',(-2.24377966520614,-7.29268000202141,
5.35034515697271));
#36645=CARTESIAN_POINT('Ctrl Pts',(-2.28292596337488,-6.30201503000759,
6.48797786134668));
#36646=CARTESIAN_POINT('Ctrl Pts',(-2.32207226154363,-5.10142365877174,
7.32420712829358));
#36647=CARTESIAN_POINT('Ctrl Pts',(-2.36121855971237,-3.9008322875359,8.16043639524047));
#36648=CARTESIAN_POINT('Ctrl Pts',(-2.40036485788111,-2.49031451707803,
8.69526222476028));
#36649=CARTESIAN_POINT('Ctrl Pts',(-2.43951115604986,-1.0371146030729,8.86526669949332));
#36650=CARTESIAN_POINT('Ctrl Pts',(-2.4786574542186,0.416085310932213,9.03527117422634));
#36651=CARTESIAN_POINT('Ctrl Pts',(-2.51780375238735,1.91196736848452,8.84045429417261));
#36652=CARTESIAN_POINT('Ctrl Pts',(-2.55695005055609,3.27315197002397,8.30391690262062));
#36653=CARTESIAN_POINT('Ctrl Pts',(-2.59609634872483,4.63433657156346,7.76737951106861));
#36654=CARTESIAN_POINT('Ctrl Pts',(-2.63524264689358,5.86082371709005,6.88912160801828));
#36655=CARTESIAN_POINT('Ctrl Pts',(-2.67438894506232,6.80718418858864,5.77328301450695));
#36656=CARTESIAN_POINT('Ctrl Pts',(-2.71353524323107,7.7535446600872,4.65744442099566));
#36657=CARTESIAN_POINT('Ctrl Pts',(-2.75268154139981,8.41977845755782,3.30402513702336));
#36658=CARTESIAN_POINT('Ctrl Pts',(-2.79182783956856,8.7268853455449,1.87350777816278));
#36659=CARTESIAN_POINT('Ctrl Pts',(-2.8309741377373,9.03399223353197,0.442990419302195));
#36660=CARTESIAN_POINT('Ctrl Pts',(-2.87012043590604,8.9819722120355,-1.06462501444667));
#36661=CARTESIAN_POINT('Ctrl Pts',(-2.90926673407479,8.57699417009785,-2.47057212345786));
#36662=CARTESIAN_POINT('Ctrl Pts',(-2.94841303224353,8.17201612816018,-3.87651923246909));
#36663=CARTESIAN_POINT('Ctrl Pts',(-2.98755933041227,7.41408006578131,-5.18079801674265));
#36664=CARTESIAN_POINT('Ctrl Pts',(-3.02670562858102,6.39305842845737,-6.22875278545715));
#36665=CARTESIAN_POINT('Ctrl Pts',(-3.06585192674976,5.37203679113344,-7.27670755417164));
#36666=CARTESIAN_POINT('Ctrl Pts',(-3.10499822491851,4.08792957886444,-8.06833830732709));
#36667=CARTESIAN_POINT('Ctrl Pts',(-3.14414452308726,2.69300075528545,-8.50977694516169));
#36668=CARTESIAN_POINT('Ctrl Pts',(-3.183290821256,1.29807193170646,-8.95121558299629));
#36669=CARTESIAN_POINT('Ctrl Pts',(-3.22243711942474,-0.207678503182533,
-9.04246210551005));
#36670=CARTESIAN_POINT('Ctrl Pts',(-3.26158341759348,-1.64570532879268,
-8.77269689408073));
#36671=CARTESIAN_POINT('Ctrl Pts',(-3.30072971576223,-3.08373215440282,
-8.50293168265141));
#36672=CARTESIAN_POINT('Ctrl Pts',(-3.33987601393097,-4.45403537073412,
-7.87215473727899));
#36673=CARTESIAN_POINT('Ctrl Pts',(-3.37902231209972,-5.59413038066898,
-6.95516083031861));
#36674=CARTESIAN_POINT('Ctrl Pts',(-3.41816861026846,-6.73422539060384,
-6.03816692335823));
#36675=CARTESIAN_POINT('Ctrl Pts',(-3.45731490843721,-7.64411219414225,
-4.83495605480989));
#36676=CARTESIAN_POINT('Ctrl Pts',(-3.49646120660595,-8.21590041578719,
-3.4881997023796));
#36677=CARTESIAN_POINT('Ctrl Pts',(-3.52841186261556,-8.68258589141955,
-2.38899617718856));
#36678=CARTESIAN_POINT('Ctrl Pts',(-3.56036251862518,-8.92404381905845,
-1.19416847877798));
#36679=CARTESIAN_POINT('Ctrl Pts',(-3.59231317463479,-8.92520804921716,
0.00020252989606076));
#36680=CARTESIAN_POINT('Ctrl Pts',(-3.80768682536521,-8.9253958274169,0.000172963988443203));
#36681=CARTESIAN_POINT('Ctrl Pts',(-3.77398923960428,-8.92427921952252,
-1.25942469024143));
#36682=CARTESIAN_POINT('Ctrl Pts',(-3.74029165384335,-8.65488294674644,
-2.51948496306796));
#36683=CARTESIAN_POINT('Ctrl Pts',(-3.70659406808243,-8.13735199258016,
-3.66770482771282));
#36684=CARTESIAN_POINT('Ctrl Pts',(-3.66744776991368,-7.53613915831117,
-5.00158546544041));
#36685=CARTESIAN_POINT('Ctrl Pts',(-3.62830147174494,-6.60006013934619,
-6.18453367174483));
#36686=CARTESIAN_POINT('Ctrl Pts',(-3.58915517357619,-5.44011108944268,
-7.07628062528088));
#36687=CARTESIAN_POINT('Ctrl Pts',(-3.55000887540745,-4.28016203953921,
-7.9680275788169));
#36688=CARTESIAN_POINT('Ctrl Pts',(-3.51086257723871,-2.89634295869721,
-8.56857327958457));
#36689=CARTESIAN_POINT('Ctrl Pts',(-3.47171627906996,-1.45274105673856,
-8.80670764676786));
#36690=CARTESIAN_POINT('Ctrl Pts',(-3.43256998090122,-0.00913915477988414,
-9.04484201395115));
#36691=CARTESIAN_POINT('Ctrl Pts',(-3.39342368273248,1.49424556829545,-8.92056504755005));
#36692=CARTESIAN_POINT('Ctrl Pts',(-3.35427738456373,2.87914833012853,-8.44861296604076));
#36693=CARTESIAN_POINT('Ctrl Pts',(-3.31513108639499,4.26405109196163,-7.97666088453146));
#36694=CARTESIAN_POINT('Ctrl Pts',(-3.27598478822624,5.53047189255247,-7.15703368791396));
#36695=CARTESIAN_POINT('Ctrl Pts',(-3.23683849005749,6.52824409825605,-6.08691918277787));
#36696=CARTESIAN_POINT('Ctrl Pts',(-3.19769219188875,7.52601630395961,-5.01680467764181));
#36697=CARTESIAN_POINT('Ctrl Pts',(-3.15854589372001,8.25513991477593,-3.69620286398717));
#36698=CARTESIAN_POINT('Ctrl Pts',(-3.11939959555127,8.62915863886055,-2.2817049241895));
#36699=CARTESIAN_POINT('Ctrl Pts',(-3.08025329738252,9.00317736294517,-0.86720698439182));
#36700=CARTESIAN_POINT('Ctrl Pts',(-3.04110699921378,9.02209120029809,0.641187081548901));
#36701=CARTESIAN_POINT('Ctrl Pts',(-3.00196070104503,8.68365744070487,2.06461850420449));
#36702=CARTESIAN_POINT('Ctrl Pts',(-2.96281440287629,8.34522368111165,3.4880499268601));
#36703=CARTESIAN_POINT('Ctrl Pts',(-2.92366810470755,7.64944232457228,4.82651870623058));
#36704=CARTESIAN_POINT('Ctrl Pts',(-2.8845218065388,6.67881605995841,5.92131507685209));
#36705=CARTESIAN_POINT('Ctrl Pts',(-2.84537550837006,5.70818979534454,7.01611144747359));
#36706=CARTESIAN_POINT('Ctrl Pts',(-2.80622921020131,4.46271862265616,7.86723540934612));
#36707=CARTESIAN_POINT('Ctrl Pts',(-2.76708291203257,3.09008510102932,8.37376439859726));
#36708=CARTESIAN_POINT('Ctrl Pts',(-2.72793661386383,1.71745157940249,8.88029338784841));
#36709=CARTESIAN_POINT('Ctrl Pts',(-2.68879031569508,0.217655708837203,
9.04222740447817));
#36710=CARTESIAN_POINT('Ctrl Pts',(-2.64964401752634,-1.23146335510331,
8.84036503982962));
#36711=CARTESIAN_POINT('Ctrl Pts',(-2.61049771935759,-2.68058241904383,
8.63850267518107));
#36712=CARTESIAN_POINT('Ctrl Pts',(-2.57135142118885,-4.07902467635957,
8.07284392925421));
#36713=CARTESIAN_POINT('Ctrl Pts',(-2.5322051230201,-5.26096881651629,7.21046210448127));
#36714=CARTESIAN_POINT('Ctrl Pts',(-2.49305882485136,-6.442912956673,6.34808027970835));
#36715=CARTESIAN_POINT('Ctrl Pts',(-2.45391252668262,-7.40835897967068,
5.18897537608936));
#36716=CARTESIAN_POINT('Ctrl Pts',(-2.41476622851387,-8.04282881216971,
3.87058905149697));
#36717=CARTESIAN_POINT('Ctrl Pts',(-2.37907309413098,-8.62133094526183,
2.66849990249503));
#36718=CARTESIAN_POINT('Ctrl Pts',(-2.34337995974809,-8.92467344142811,
1.33399090208915));
#36719=CARTESIAN_POINT('Ctrl Pts',(-2.3076868253652,-8.92557695889132,-0.000120900814251108));
#36720=CARTESIAN_POINT('Origin',(-14.3478126690739,0.,0.));
#36721=CARTESIAN_POINT('',(-1.59781266907387,-8.06911106248246,-5.74742776433716E-5));
#36722=CARTESIAN_POINT('',(-1.5,-8.0685,-1.61713948722842E-13));
#36723=CARTESIAN_POINT('',(-14.3478126690739,-8.0685,-1.61713948722842E-13));
#36724=CARTESIAN_POINT('',(-1.5,-7.40070004445565,-3.21408324440955));
#36725=CARTESIAN_POINT('Ctrl Pts',(-1.59781266907387,-8.06911106248246,
-5.74742776435905E-5));
#36726=CARTESIAN_POINT('Ctrl Pts',(-1.59610643503933,-8.06913365948742,
-0.0577095977506832));
#36727=CARTESIAN_POINT('Ctrl Pts',(-1.56350221201471,-8.05757148270878,
-1.15936810984891));
#36728=CARTESIAN_POINT('Ctrl Pts',(-1.53089798899008,-7.81573019911042,
-2.25608704898405));
#36729=CARTESIAN_POINT('Ctrl Pts',(-1.5,-7.40071554151276,-3.21429017473183));
#36730=CARTESIAN_POINT('Origin',(-1.5,0.,0.));
#36731=CARTESIAN_POINT('Origin',(-14.3478126690739,0.,0.));
#36732=CARTESIAN_POINT('',(-3.09781266907387,-8.06868808348557,0.000183093833578688));
#36733=CARTESIAN_POINT('',(-2.80218733092611,-8.06902159023133,-0.000109298400164937));
#36734=CARTESIAN_POINT('',(-14.3478126690739,-8.0685,-1.61713948722842E-13));
#36735=CARTESIAN_POINT('Ctrl Pts',(-3.09781266907387,-8.06868808348557,
0.000183093833578535));
#36736=CARTESIAN_POINT('Ctrl Pts',(-3.06586201306426,-8.06763558028828,
-1.07956844493236));
#36737=CARTESIAN_POINT('Ctrl Pts',(-2.9947650588859,-7.58190296737274,-3.48316225362576));
#36738=CARTESIAN_POINT('Ctrl Pts',(-2.8845218065388,-5.26539785879409,-6.54644893154043));
#36739=CARTESIAN_POINT('Ctrl Pts',(-2.76708291203257,-1.54899735426666,
-8.25717961514961));
#36740=CARTESIAN_POINT('Ctrl Pts',(-2.64964401752634,2.53474966553227,-8.00970984476226));
#36741=CARTESIAN_POINT('Ctrl Pts',(-2.5322051230201,6.01737791500869,-5.86272741389347));
#36742=CARTESIAN_POINT('Ctrl Pts',(-2.41476622851387,8.07297694670747,-2.3253918270326));
#36743=CARTESIAN_POINT('Ctrl Pts',(-2.29732733400764,8.21406049072235,1.76341325774147));
#36744=CARTESIAN_POINT('Ctrl Pts',(-2.17988843950141,6.4071672487419,5.43402283512993));
#36745=CARTESIAN_POINT('Ctrl Pts',(-2.06244954499518,3.08081043069796,7.81594683202442));
#36746=CARTESIAN_POINT('Ctrl Pts',(-1.94501065048894,-0.976172554633629,
8.34430985612986));
#36747=CARTESIAN_POINT('Ctrl Pts',(-1.82757175598271,-4.80163898520143,
6.89380827445569));
#36748=CARTESIAN_POINT('Ctrl Pts',(-1.71183909551102,-7.44938682960104,
3.85326013172529));
#36749=CARTESIAN_POINT('Ctrl Pts',(-1.63525273320807,-8.06861521414156,
1.26500883937235));
#36750=CARTESIAN_POINT('Ctrl Pts',(-1.59781266907387,-8.06911106248246,
-5.74742776435905E-5));
#36751=CARTESIAN_POINT('',(-1.5,-5.45359047959038,5.94634704090849));
#36752=CARTESIAN_POINT('Origin',(-1.5,0.,0.));
#36753=CARTESIAN_POINT('Ctrl Pts',(-2.80218733092611,-8.06902159023132,
-0.000109298400165197));
#36754=CARTESIAN_POINT('Ctrl Pts',(-2.79873416714026,-8.06910061325082,
-0.11679275755619));
#36755=CARTESIAN_POINT('Ctrl Pts',(-2.75613470518566,-8.03850549293377,
-1.55620012847858));
#36756=CARTESIAN_POINT('Ctrl Pts',(-2.67438894506232,-7.2259267400895,-4.28560128601273));
#36757=CARTESIAN_POINT('Ctrl Pts',(-2.55695005055609,-4.34491343911961,
-7.1904203216184));
#36758=CARTESIAN_POINT('Ctrl Pts',(-2.43951115604986,-0.433490517027392,
-8.39002416011216));
#36759=CARTESIAN_POINT('Ctrl Pts',(-2.32207226154363,3.58071951422406,-7.59991946597854));
#36760=CARTESIAN_POINT('Ctrl Pts',(-2.20463336703739,6.74578836548944,-5.00749194802054));
#36761=CARTESIAN_POINT('Ctrl Pts',(-2.08719447253116,8.31102423036551,-1.22751659427962));
#36762=CARTESIAN_POINT('Ctrl Pts',(-1.96975557802493,7.90541015591722,2.84353655923596));
#36763=CARTESIAN_POINT('Ctrl Pts',(-1.8523166835187,5.62478208560713,6.24029926664823));
#36764=CARTESIAN_POINT('Ctrl Pts',(-1.73487778901246,2.01069766784778,8.15705187872645));
#36765=CARTESIAN_POINT('Ctrl Pts',(-1.61743889450623,-2.08118048114745,
8.1395942446814));
#36766=CARTESIAN_POINT('Ctrl Pts',(-1.53914629816874,-4.4785344754388,6.8406029773222));
#36767=CARTESIAN_POINT('Ctrl Pts',(-1.5,-5.45359047959038,5.94634704090849));
#36768=CARTESIAN_POINT('Origin',(-14.3478126690739,0.,0.));
#36769=CARTESIAN_POINT('',(-4.59781266907387,-8.06793026735018,9.89360780153199E-5));
#36770=CARTESIAN_POINT('',(-4.30218733092611,-8.06885784129,0.000156365259223884));
#36771=CARTESIAN_POINT('',(-14.3478126690739,-8.0685,-1.61713948722842E-13));
#36772=CARTESIAN_POINT('Ctrl Pts',(-4.59781266907387,-8.06793026735018,
9.89360780155601E-5));
#36773=CARTESIAN_POINT('Ctrl Pts',(-4.57476388925793,-8.0675839294048,-0.779029920072743));
#36774=CARTESIAN_POINT('Ctrl Pts',(-4.51256881127325,-7.76507243369392,
-2.88170300903797));
#36775=CARTESIAN_POINT('Ctrl Pts',(-4.41122743511982,-5.96327500496155,
-5.91774951138349));
#36776=CARTESIAN_POINT('Ctrl Pts',(-4.29378854061358,-2.46107389287582,
-8.03265356891045));
#36777=CARTESIAN_POINT('Ctrl Pts',(-4.17634964610736,1.62477396243877,-8.24260381404624));
#36778=CARTESIAN_POINT('Ctrl Pts',(-4.05891075160112,5.32530464606164,-6.49781028429742));
#36779=CARTESIAN_POINT('Ctrl Pts',(-3.94147185709489,7.76293269109889,-3.21205294140231));
#36780=CARTESIAN_POINT('Ctrl Pts',(-3.82403296258866,8.35957156616068,0.835446762709816));
#36781=CARTESIAN_POINT('Ctrl Pts',(-3.70659406808243,6.97372761835372,4.68481922503354));
#36782=CARTESIAN_POINT('Ctrl Pts',(-3.58915517357619,3.93405546743286,7.42318096516021));
#36783=CARTESIAN_POINT('Ctrl Pts',(-3.47171627906997,-0.0385828430310631,
8.40112608093868));
#36784=CARTESIAN_POINT('Ctrl Pts',(-3.35427738456373,-4.00207118653311,
7.38673366869508));
#36785=CARTESIAN_POINT('Ctrl Pts',(-3.2368384900575,-7.01646335196947,4.620568153675));
#36786=CARTESIAN_POINT('Ctrl Pts',(-3.15135025156088,-7.99949209086729,
1.80931584281257));
#36787=CARTESIAN_POINT('Ctrl Pts',(-3.105008311233,-8.06892511888092,0.243355117950805));
#36788=CARTESIAN_POINT('Ctrl Pts',(-3.09781266907387,-8.06868808348557,
0.000183093833578535));
#36789=CARTESIAN_POINT('Ctrl Pts',(-4.30218733092611,-8.06885784129,0.000156365259223988));
#36790=CARTESIAN_POINT('Ctrl Pts',(-4.26848974516519,-8.06784839022042,
-1.13856225358147));
#36791=CARTESIAN_POINT('Ctrl Pts',(-4.19564586123552,-7.54138222205796,
-3.60102803550426));
#36792=CARTESIAN_POINT('Ctrl Pts',(-4.08365567913712,-5.12042931874465,
-6.66045126420618));
#36793=CARTESIAN_POINT('Ctrl Pts',(-3.96621678463087,-1.36737242671985,
-8.28919176391845));
#36794=CARTESIAN_POINT('Ctrl Pts',(-3.84877789012465,2.70995854408127,-7.9521400989076));
#36795=CARTESIAN_POINT('Ctrl Pts',(-3.73133899561841,6.14461946158279,-5.72922849019895));
#36796=CARTESIAN_POINT('Ctrl Pts',(-3.61390010111218,8.12207621918668,-2.14762320163677));
#36797=CARTESIAN_POINT('Ctrl Pts',(-3.49646120660595,8.17337245336549,1.94329361215914));
#36798=CARTESIAN_POINT('Ctrl Pts',(-3.37902231209972,6.28634325160488,5.57335591345347));
#36799=CARTESIAN_POINT('Ctrl Pts',(-3.26158341759348,2.90849983754228,7.88168992567818));
#36800=CARTESIAN_POINT('Ctrl Pts',(-3.14414452308725,-1.1590978033505,8.32087130825875));
#36801=CARTESIAN_POINT('Ctrl Pts',(-3.02670562858102,-4.95181422457809,
6.78674774808702));
#36802=CARTESIAN_POINT('Ctrl Pts',(-2.91271989786064,-7.49321035547616,
3.73557280180067));
#36803=CARTESIAN_POINT('Ctrl Pts',(-2.837880465309,-8.06820478007428,1.20597261551876));
#36804=CARTESIAN_POINT('Ctrl Pts',(-2.80218733092611,-8.06902159023132,
-0.000109298400165197));
#36805=CARTESIAN_POINT('Origin',(-14.3478126690739,0.,0.));
#36806=CARTESIAN_POINT('',(-6.09781266907388,-8.06804319777117,-0.000144302944734027));
#36807=CARTESIAN_POINT('',(-5.80218733092611,-8.06802936020891,0.00014009232313511));
#36808=CARTESIAN_POINT('',(-14.3478126690739,-8.0685,-1.61713948722842E-13));
#36809=CARTESIAN_POINT('Ctrl Pts',(-6.09781266907388,-8.06804319777117,
-0.000144302944733825));
#36810=CARTESIAN_POINT('Ctrl Pts',(-6.08366576545161,-8.06835928950991,
-0.478339617312313));
#36811=CARTESIAN_POINT('Ctrl Pts',(-6.0303725636606,-7.91071536051216,-2.27955671366496));
#36812=CARTESIAN_POINT('Ctrl Pts',(-5.93793306370085,-6.58660781722385,
-5.21507483420824));
#36813=CARTESIAN_POINT('Ctrl Pts',(-5.8204941691946,-3.34238556640572,-7.70771475794147));
#36814=CARTESIAN_POINT('Ctrl Pts',(-5.70305527468838,0.694487590192009,
-8.37246051357519));
#36815=CARTESIAN_POINT('Ctrl Pts',(-5.58561638018214,4.56666214859352,-7.0516668160733));
#36816=CARTESIAN_POINT('Ctrl Pts',(-5.46817748567591,7.35584708280132,-4.05856153812523));
#36817=CARTESIAN_POINT('Ctrl Pts',(-5.35073859116968,8.40058370692718,-0.102963329471767));
#36818=CARTESIAN_POINT('Ctrl Pts',(-5.23329969666345,7.45311142753807,3.87705276118435));
#36819=CARTESIAN_POINT('Ctrl Pts',(-5.11586080215721,4.73812447740229,6.93762095396888));
#36820=CARTESIAN_POINT('Ctrl Pts',(-4.99842190765099,0.89948539794352,8.35292368474611));
#36821=CARTESIAN_POINT('Ctrl Pts',(-4.88098301314475,-3.15246776549777,
7.7873201457114));
#36822=CARTESIAN_POINT('Ctrl Pts',(-4.76354411863852,-6.45680926651568,
5.37494392158168));
#36823=CARTESIAN_POINT('Ctrl Pts',(-4.66915400394823,-7.88191821152657,
2.41152062990943));
#36824=CARTESIAN_POINT('Ctrl Pts',(-4.61391018742668,-8.06817215353576,
0.544250997976407));
#36825=CARTESIAN_POINT('Ctrl Pts',(-4.59781266907387,-8.06793026735018,
9.89360780155601E-5));
#36826=CARTESIAN_POINT('Ctrl Pts',(-5.80218733092611,-8.06802936020891,
0.00014009232313518));
#36827=CARTESIAN_POINT('Ctrl Pts',(-5.77739162135886,-8.06749280865517,
-0.838011532852666));
#36828=CARTESIAN_POINT('Ctrl Pts',(-5.71344961362287,-7.73214656047648,
-2.99981704381613));
#36829=CARTESIAN_POINT('Ctrl Pts',(-5.61036130771812,-5.83193878421242,
-6.0472222937725));
#36830=CARTESIAN_POINT('Ctrl Pts',(-5.49292241321191,-2.28415769210351,
-8.08474063224692));
#36831=CARTESIAN_POINT('Ctrl Pts',(-5.37548351870566,1.80531424554574,-8.20495264629408));
#36832=CARTESIAN_POINT('Ctrl Pts',(-5.25804462419944,5.46665365823166,-6.37934990685156));
#36833=CARTESIAN_POINT('Ctrl Pts',(-5.14060572969319,7.83156933772,-3.0408763805148));
#36834=CARTESIAN_POINT('Ctrl Pts',(-5.02316683518698,8.3392185810425,1.01874477211711));
#36835=CARTESIAN_POINT('Ctrl Pts',(-4.90572794068073,6.86921173698437,4.83676933143891));
#36836=CARTESIAN_POINT('Ctrl Pts',(-4.78828904617451,3.770162762059,7.50774801126825));
#36837=CARTESIAN_POINT('Ctrl Pts',(-4.67085015166827,-0.222985014150146,
8.39825488638014));
#36838=CARTESIAN_POINT('Ctrl Pts',(-4.55341125716204,-4.16325161610056,
7.29710514066449));
#36839=CARTESIAN_POINT('Ctrl Pts',(-4.43597236265581,-7.1161979048615,4.46543780972854));
#36840=CARTESIAN_POINT('Ctrl Pts',(-4.3522310539105,-8.0184584470612,1.69115891412015));
#36841=CARTESIAN_POINT('Ctrl Pts',(-4.30763604333393,-8.06902106391987,
0.18428083968042));
#36842=CARTESIAN_POINT('Ctrl Pts',(-4.30218733092611,-8.06885784129,0.000156365259223988));
#36843=CARTESIAN_POINT('Origin',(-14.3478126690739,0.,0.));
#36844=CARTESIAN_POINT('',(-7.59781266907388,-8.06887641478357,-0.000152324058379699));
#36845=CARTESIAN_POINT('',(-7.30218733092611,-8.06793992440636,-0.000104148435049745));
#36846=CARTESIAN_POINT('',(-14.3478126690739,-8.0685,-1.61713948722842E-13));
#36847=CARTESIAN_POINT('Ctrl Pts',(-7.59781266907388,-8.06887641478357,
-0.000152324058379522));
#36848=CARTESIAN_POINT('Ctrl Pts',(-7.59256764164528,-8.06903072901403,
-0.177392638492444));
#36849=CARTESIAN_POINT('Ctrl Pts',(-7.54817631604794,-8.02058356892345,
-1.67738301722052));
#36850=CARTESIAN_POINT('Ctrl Pts',(-7.46463869228187,-7.12760426199033,
-4.44720873681053));
#36851=CARTESIAN_POINT('Ctrl Pts',(-7.34719979777563,-4.18191550738002,
-7.28642510106571));
#36852=CARTESIAN_POINT('Ctrl Pts',(-7.2297609032694,-0.244480274405397,
-8.39765666479245));
#36853=CARTESIAN_POINT('Ctrl Pts',(-7.11232200876316,3.75093376056635,-7.51737347669715));
#36854=CARTESIAN_POINT('Ctrl Pts',(-6.99488311425694,6.85680917596183,-4.85433579274776));
#36855=CARTESIAN_POINT('Ctrl Pts',(-6.8774442197507,8.33658374329481,-1.04008632109978));
#36856=CARTESIAN_POINT('Ctrl Pts',(-6.76000532524447,7.83932707831064,3.02082091881856));
#36857=CARTESIAN_POINT('Ctrl Pts',(-6.64256643073823,5.48296421930119,6.36533671019601));
#36858=CARTESIAN_POINT('Ctrl Pts',(-6.52512753623201,1.82630955719499,8.20030496174408));
#36859=CARTESIAN_POINT('Ctrl Pts',(-6.40768864172577,-2.26345669421878,
8.09056066399));
#36860=CARTESIAN_POINT('Ctrl Pts',(-6.29024974721954,-5.81644136755901,
6.06212981402202));
#36861=CARTESIAN_POINT('Ctrl Pts',(-6.18695775633558,-7.72821288647723,
3.01358673818511));
#36862=CARTESIAN_POINT('Ctrl Pts',(-6.12281206362035,-8.0674846230964,0.844888196982259));
#36863=CARTESIAN_POINT('Ctrl Pts',(-6.09781266907388,-8.06804319777117,
-0.000144302944733825));
#36864=CARTESIAN_POINT('Ctrl Pts',(-7.30218733092611,-8.06793992440636,
-0.000104148435049883));
#36865=CARTESIAN_POINT('Ctrl Pts',(-7.28629349755254,-8.06819173593772,
-0.537369098197992));
#36866=CARTESIAN_POINT('Ctrl Pts',(-7.23125336601021,-7.88500596100739,
-2.39774097328042));
#36867=CARTESIAN_POINT('Ctrl Pts',(-7.13706693629915,-6.47054567674393,
-5.35839958366958));
#36868=CARTESIAN_POINT('Ctrl Pts',(-7.01962804179292,-3.17238967957803,
-7.77922561531716));
#36869=CARTESIAN_POINT('Ctrl Pts',(-6.90218914728668,0.878102486783198,
-8.35519858984843));
#36870=CARTESIAN_POINT('Ctrl Pts',(-6.78475025278046,4.72035155321251,-6.94972579798543));
#36871=CARTESIAN_POINT('Ctrl Pts',(-6.66731135827422,7.4431633614575,-3.89611686525913));
#36872=CARTESIAN_POINT('Ctrl Pts',(-6.54987246376799,8.40081969523418,0.0814610413973314));
#36873=CARTESIAN_POINT('Ctrl Pts',(-6.43243356926176,7.36621116057458,4.03972036048615));
#36874=CARTESIAN_POINT('Ctrl Pts',(-6.31499467475553,4.58469646186278,7.03995495764589));
#36875=CARTESIAN_POINT('Ctrl Pts',(-6.1975557802493,0.715915279072651,8.3706554561928));
#36876=CARTESIAN_POINT('Ctrl Pts',(-6.08011688574306,-3.32264610505695,
7.71624457321371));
#36877=CARTESIAN_POINT('Ctrl Pts',(-5.96267799123684,-6.57323782128532,
5.23191666580462));
#36878=CARTESIAN_POINT('Ctrl Pts',(-5.87003480629784,-7.90778884858942,
2.29333657883371));
#36879=CARTESIAN_POINT('Ctrl Pts',(-5.8165379195276,-8.06833989097192,0.485222768660689));
#36880=CARTESIAN_POINT('Ctrl Pts',(-5.80218733092611,-8.06802936020891,
0.00014009232313518));
#36881=CARTESIAN_POINT('Origin',(-14.3478126690739,0.,0.));
#36882=CARTESIAN_POINT('',(-9.09781266907388,-8.0690069255314,0.000114842546288661));
#36883=CARTESIAN_POINT('',(-8.80218733092612,-8.06870858189138,-0.000180733618864171));
#36884=CARTESIAN_POINT('',(-14.3478126690739,-8.0685,-1.61713948722842E-13));
#36885=CARTESIAN_POINT('Ctrl Pts',(-9.09781266907388,-8.0690069255314,0.000114842546288605));
#36886=CARTESIAN_POINT('Ctrl Pts',(-9.06232321967021,-8.06816227230134,
-1.19909076398325));
#36887=CARTESIAN_POINT('Ctrl Pts',(-8.9876874720978,-7.4982202312652,-3.7218450346353));
#36888=CARTESIAN_POINT('Ctrl Pts',(-8.87390542635665,-4.96916911103115,
-6.77405096026056));
#36889=CARTESIAN_POINT('Ctrl Pts',(-8.75646653185041,-1.18039199564904,
-8.31787730131265));
#36890=CARTESIAN_POINT('Ctrl Pts',(-8.63902763734419,2.88831655372436,-7.88910866640744));
#36891=CARTESIAN_POINT('Ctrl Pts',(-8.52158874283795,6.27205722999723,-5.5894280716122));
#36892=CARTESIAN_POINT('Ctrl Pts',(-8.40414984833172,8.16837171151259,-1.96420763844087));
#36893=CARTESIAN_POINT('Ctrl Pts',(-8.28671095382549,8.12754665384501,2.12682708603627));
#36894=CARTESIAN_POINT('Ctrl Pts',(-8.16927205931926,6.15926377034014,5.71348211440747));
#36895=CARTESIAN_POINT('Ctrl Pts',(-8.05183316481303,2.73030380171169,7.94517773336033));
#36896=CARTESIAN_POINT('Ctrl Pts',(-7.93439427030679,-1.34615111879544,
8.29266454341796));
#36897=CARTESIAN_POINT('Ctrl Pts',(-7.81695537580056,-5.1033646225271,6.67353561418904));
#36898=CARTESIAN_POINT('Ctrl Pts',(-7.70476150872293,-7.53655783590869,
3.61476589733093));
#36899=CARTESIAN_POINT('Ctrl Pts',(-7.63171393981403,-8.06787900369719,
1.14544166329457));
#36900=CARTESIAN_POINT('Ctrl Pts',(-7.59781266907388,-8.06887641478357,
-0.000152324058379522));
#36901=CARTESIAN_POINT('Ctrl Pts',(-8.80218733092612,-8.06870858189138,
-0.000180733618863893));
#36902=CARTESIAN_POINT('Ctrl Pts',(-8.79519537374621,-8.06893746644687,
-0.236467619644774));
#36903=CARTESIAN_POINT('Ctrl Pts',(-8.74905711839756,-8.00177191450951,
-1.79553866882014));
#36904=CARTESIAN_POINT('Ctrl Pts',(-8.66377256488016,-7.02826704496481,
-4.60259381194273));
#36905=CARTESIAN_POINT('Ctrl Pts',(-8.54633367037395,-4.02096498037294,
-7.37646582583656));
#36906=CARTESIAN_POINT('Ctrl Pts',(-8.4288947758677,-0.0600860556372529,
-8.400999769016));
#36907=CARTESIAN_POINT('Ctrl Pts',(-8.31145588136148,3.91504235213327,-7.43322613904));
#36908=CARTESIAN_POINT('Ctrl Pts',(-8.19401698685524,6.96171358315727,-4.70265365928452));
#36909=CARTESIAN_POINT('Ctrl Pts',(-8.07657809234901,8.35740575511295,-0.856840998963709));
#36910=CARTESIAN_POINT('Ctrl Pts',(-7.95913919784278,7.77112872867905,3.19217257293514));
#36911=CARTESIAN_POINT('Ctrl Pts',(-7.84170030333654,5.34191883189369,6.48415843780511));
#36912=CARTESIAN_POINT('Ctrl Pts',(-7.72426140883031,1.64586622155058,8.23841804194586));
#36913=CARTESIAN_POINT('Ctrl Pts',(-7.60682251432408,-2.44050561599858,
8.038926532279));
#36914=CARTESIAN_POINT('Ctrl Pts',(-7.48938361981785,-5.94810850285432,
5.93299356913289));
#36915=CARTESIAN_POINT('Ctrl Pts',(-7.38783855868519,-7.76130804072777,
2.895476037464));
#36916=CARTESIAN_POINT('Ctrl Pts',(-7.32543979572128,-8.06757152751744,
0.785907258404543));
#36917=CARTESIAN_POINT('Ctrl Pts',(-7.30218733092611,-8.06793992440636,
-0.000104148435049883));
#36918=CARTESIAN_POINT('Origin',(-14.3478126690739,0.,0.));
#36919=CARTESIAN_POINT('',(-10.5978126690739,-8.06816497465237,0.000173167597293405));
#36920=CARTESIAN_POINT('',(-10.3021873309261,-8.06911057618467,6.34335902039915E-5));
#36921=CARTESIAN_POINT('',(-14.3478126690739,-8.0685,-1.61713948722842E-13));
#36922=CARTESIAN_POINT('Ctrl Pts',(-10.5978126690739,-8.06816497465237,
0.000173167597293036));
#36923=CARTESIAN_POINT('Ctrl Pts',(-10.5712250958639,-8.06744060058938,
-0.898504524201405));
#36924=CARTESIAN_POINT('Ctrl Pts',(-10.5054912244852,-7.69685793866654,
-3.12093756422147));
#36925=CARTESIAN_POINT('Ctrl Pts',(-10.4006110549377,-5.69430528428376,
-6.17699632956363));
#36926=CARTESIAN_POINT('Ctrl Pts',(-10.2831721604314,-2.10154812737837,
-8.1341202063368));
#36927=CARTESIAN_POINT('Ctrl Pts',(-10.1657332659252,1.98959372976295,-8.16222523101317));
#36928=CARTESIAN_POINT('Ctrl Pts',(-10.048294371419,5.60890098251375,-6.25464942822609));
#36929=CARTESIAN_POINT('Ctrl Pts',(-9.93085547691274,7.89805035642209,-2.86377517127619));
#36930=CARTESIAN_POINT('Ctrl Pts',(-9.8134165824065,8.31416724541664,1.20624666449639));
#36931=CARTESIAN_POINT('Ctrl Pts',(-9.69597768790028,6.75856899858617,4.99020573884583));
#36932=CARTESIAN_POINT('Ctrl Pts',(-9.57853879339404,3.60016768628482,7.59073122748412));
#36933=CARTESIAN_POINT('Ctrl Pts',(-9.46109989888781,-0.412017884052814,
8.3911053741381));
#36934=CARTESIAN_POINT('Ctrl Pts',(-9.34366100438158,-4.32649289879303,
7.20151839746173));
#36935=CARTESIAN_POINT('Ctrl Pts',(-9.22622210987535,-7.21493472673645,
4.30408236018371));
#36936=CARTESIAN_POINT('Ctrl Pts',(-9.14427266477278,-8.03653802371325,
1.56997461945975));
#36937=CARTESIAN_POINT('Ctrl Pts',(-9.10146951783896,-8.06909395897861,
0.123681525461907));
#36938=CARTESIAN_POINT('Ctrl Pts',(-9.09781266907388,-8.0690069255314,0.000114842546288605));
#36939=CARTESIAN_POINT('Ctrl Pts',(-10.3021873309261,-8.06911057618467,
6.34335902037139E-5));
#36940=CARTESIAN_POINT('Ctrl Pts',(-10.2649509517711,-8.0685730995522,-1.25812477433403));
#36941=CARTESIAN_POINT('Ctrl Pts',(-10.1885682744474,-7.45456459945451,
-3.839542418202));
#36942=CARTESIAN_POINT('Ctrl Pts',(-10.073039298955,-4.81927591637304,-6.88149598316814));
#36943=CARTESIAN_POINT('Ctrl Pts',(-9.95560040444872,-0.997523488572918,
-8.34178364717233));
#36944=CARTESIAN_POINT('Ctrl Pts',(-9.83816150994251,3.06079288122268,-7.82380689682625));
#36945=CARTESIAN_POINT('Ctrl Pts',(-9.72072261543626,6.39323840044666,-5.45040459216995));
#36946=CARTESIAN_POINT('Ctrl Pts',(-9.60328372093004,8.20951945985529,-1.78443203586594));
#36947=CARTESIAN_POINT('Ctrl Pts',(-9.48584482642378,8.07890273990855,2.30472080092658));
#36948=CARTESIAN_POINT('Ctrl Pts',(-9.36840593191757,6.03236415915333,5.84730622649608));
#36949=CARTESIAN_POINT('Ctrl Pts',(-9.25096703741134,2.55524289425404,8.00319568692536));
#36950=CARTESIAN_POINT('Ctrl Pts',(-9.1335281429051,-1.5278574099364,8.26111730873075));
#36951=CARTESIAN_POINT('Ctrl Pts',(-9.01608924839887,-5.24862442380086,
6.55990465713925));
#36952=CARTESIAN_POINT('Ctrl Pts',(-8.90564231107254,-7.57725711709514,
3.49690855884589));
#36953=CARTESIAN_POINT('Ctrl Pts',(-8.83434167191496,-8.06765599649145,
1.08644621631508));
#36954=CARTESIAN_POINT('Ctrl Pts',(-8.80218733092612,-8.06870858189138,
-0.000180733618863893));
#36955=CARTESIAN_POINT('Origin',(9.5,-11.,5.85085296108588));
#36956=CARTESIAN_POINT('',(9.5,-10.5669872981078,6.60085296108588));
#36957=CARTESIAN_POINT('',(10.,-10.5,6.06217782649107));
#36958=CARTESIAN_POINT('',(9.5,-10.5669872981078,6.60085296108588));
#36959=CARTESIAN_POINT('',(9.5,-11.,5.85085296108588));
#36960=CARTESIAN_POINT('',(9.5,-11.,5.85085296108588));
#36961=CARTESIAN_POINT('',(10.,-10.5,6.06217782649107));
#36962=CARTESIAN_POINT('Origin',(2.,-10.7834936490539,6.22585296108588));
#36963=CARTESIAN_POINT('',(2.,-11.,5.85085296108588));
#36964=CARTESIAN_POINT('',(2.,-10.5669872981078,6.60085296108588));
#36965=CARTESIAN_POINT('',(2.,-10.7834936490539,6.22585296108588));
#36966=CARTESIAN_POINT('',(2.,-11.,5.85085296108588));
#36967=CARTESIAN_POINT('',(2.,-10.5669872981078,6.60085296108588));
#36968=CARTESIAN_POINT('Origin',(9.5,-0.433012701892219,12.4517059221718));
#36969=CARTESIAN_POINT('',(9.5,0.433012701892219,12.4517059221718));
#36970=CARTESIAN_POINT('',(10.,-1.11022302462516E-15,12.1243556529821));
#36971=CARTESIAN_POINT('',(9.5,0.433012701892218,12.4517059221718));
#36972=CARTESIAN_POINT('',(9.5,-0.433012701892218,12.4517059221718));
#36973=CARTESIAN_POINT('',(9.5,-0.433012701892219,12.4517059221718));
#36974=CARTESIAN_POINT('',(10.,1.38777878078145E-15,12.1243556529821));
#36975=CARTESIAN_POINT('Origin',(2.,1.73472347597681E-16,12.4517059221718));
#36976=CARTESIAN_POINT('',(2.,-0.433012701892219,12.4517059221718));
#36977=CARTESIAN_POINT('',(2.,0.433012701892219,12.4517059221718));
#36978=CARTESIAN_POINT('',(2.,8.67361737988404E-17,12.4517059221718));
#36979=CARTESIAN_POINT('',(2.,-0.433012701892219,12.4517059221718));
#36980=CARTESIAN_POINT('',(2.,0.433012701892219,12.4517059221718));
#36981=CARTESIAN_POINT('Origin',(9.75,-2.625,10.8974863309542));
#36982=CARTESIAN_POINT('',(10.,-2.5,10.6809799800081));
#36983=CARTESIAN_POINT('',(9.5,-2.75,11.1139926819003));
#36984=CARTESIAN_POINT('Origin',(9.5,-10.5669872981078,-6.60085296108588));
#36985=CARTESIAN_POINT('',(9.5,-11.,-5.85085296108588));
#36986=CARTESIAN_POINT('',(10.,-10.5,-6.06217782649107));
#36987=CARTESIAN_POINT('',(9.5,-11.,-5.85085296108588));
#36988=CARTESIAN_POINT('',(9.5,-10.5669872981078,-6.60085296108589));
#36989=CARTESIAN_POINT('',(9.5,-10.5669872981078,-6.60085296108588));
#36990=CARTESIAN_POINT('',(10.,-10.5,-6.06217782649107));
#36991=CARTESIAN_POINT('Origin',(2.,-10.7834936490539,-6.22585296108588));
#36992=CARTESIAN_POINT('',(2.,-10.5669872981078,-6.60085296108588));
#36993=CARTESIAN_POINT('',(2.,-11.,-5.85085296108588));
#36994=CARTESIAN_POINT('',(2.,-10.7834936490539,-6.22585296108588));
#36995=CARTESIAN_POINT('',(2.,-10.5669872981078,-6.60085296108588));
#36996=CARTESIAN_POINT('',(2.,-11.,-5.85085296108588));
#36997=CARTESIAN_POINT('Origin',(9.5,10.5669872981078,6.60085296108588));
#36998=CARTESIAN_POINT('',(9.5,11.,5.85085296108588));
#36999=CARTESIAN_POINT('',(10.,10.5,6.06217782649107));
#37000=CARTESIAN_POINT('',(9.5,11.,5.85085296108588));
#37001=CARTESIAN_POINT('',(9.5,10.5669872981078,6.60085296108588));
#37002=CARTESIAN_POINT('',(9.5,10.5669872981078,6.60085296108588));
#37003=CARTESIAN_POINT('',(10.,10.5,6.06217782649107));
#37004=CARTESIAN_POINT('Origin',(2.,10.7834936490539,6.22585296108588));
#37005=CARTESIAN_POINT('',(2.,10.5669872981078,6.60085296108588));
#37006=CARTESIAN_POINT('',(2.,11.,5.85085296108588));
#37007=CARTESIAN_POINT('',(2.,10.7834936490539,6.22585296108588));
#37008=CARTESIAN_POINT('',(2.,10.5669872981078,6.60085296108588));
#37009=CARTESIAN_POINT('',(2.,11.,5.85085296108588));
#37010=CARTESIAN_POINT('Origin',(9.75,8.125,7.72205985041124));
#37011=CARTESIAN_POINT('',(10.,8.,7.50555349946513));
#37012=CARTESIAN_POINT('',(9.5,8.25,7.93856620135735));
#37013=CARTESIAN_POINT('Origin',(9.5,0.433012701892216,-12.4517059221718));
#37014=CARTESIAN_POINT('',(9.5,-0.433012701892221,-12.4517059221718));
#37015=CARTESIAN_POINT('',(10.,-2.22044604925031E-15,-12.1243556529821));
#37016=CARTESIAN_POINT('',(9.5,-0.43301270189222,-12.4517059221718));
#37017=CARTESIAN_POINT('',(9.5,0.433012701892216,-12.4517059221718));
#37018=CARTESIAN_POINT('',(9.5,0.433012701892216,-12.4517059221718));
#37019=CARTESIAN_POINT('',(10.,-2.22044604925031E-15,-12.1243556529821));
#37020=CARTESIAN_POINT('Origin',(2.,-2.18575157973078E-15,-12.4517059221718));
#37021=CARTESIAN_POINT('',(2.,0.433012701892215,-12.4517059221718));
#37022=CARTESIAN_POINT('',(2.,-0.433012701892219,-12.4517059221718));
#37023=CARTESIAN_POINT('',(2.,-1.09287578986539E-15,-12.4517059221718));
#37024=CARTESIAN_POINT('',(2.,0.433012701892216,-12.4517059221718));
#37025=CARTESIAN_POINT('',(2.,-0.433012701892221,-12.4517059221718));
#37026=CARTESIAN_POINT('Origin',(9.5,11.,-5.85085296108589));
#37027=CARTESIAN_POINT('',(9.5,10.5669872981078,-6.60085296108589));
#37028=CARTESIAN_POINT('',(10.,10.5,-6.06217782649107));
#37029=CARTESIAN_POINT('',(9.5,10.5669872981078,-6.60085296108589));
#37030=CARTESIAN_POINT('',(9.5,11.,-5.85085296108589));
#37031=CARTESIAN_POINT('',(9.5,11.,-5.85085296108589));
#37032=CARTESIAN_POINT('',(10.,10.5,-6.06217782649108));
#37033=CARTESIAN_POINT('Origin',(2.,10.7834936490539,-6.22585296108589));
#37034=CARTESIAN_POINT('',(2.,11.,-5.85085296108589));
#37035=CARTESIAN_POINT('',(2.,10.5669872981078,-6.60085296108589));
#37036=CARTESIAN_POINT('',(2.,10.7834936490539,-6.22585296108588));
#37037=CARTESIAN_POINT('',(2.,11.,-5.85085296108589));
#37038=CARTESIAN_POINT('',(2.,10.5669872981078,-6.60085296108589));
#37039=CARTESIAN_POINT('Origin',(9.75,10.75,-3.17542648054295));
#37040=CARTESIAN_POINT('',(10.,10.5,-3.17542648054295));
#37041=CARTESIAN_POINT('',(9.5,11.,-3.17542648054295));
#37042=CARTESIAN_POINT('Origin',(9.75,2.625,-10.8974863309542));
#37043=CARTESIAN_POINT('',(10.,2.5,-10.6809799800081));
#37044=CARTESIAN_POINT('',(9.5,2.75,-11.1139926819003));
#37045=CARTESIAN_POINT('Origin',(9.75,-8.125,-7.72205985041125));
#37046=CARTESIAN_POINT('',(10.,-8.,-7.50555349946514));
#37047=CARTESIAN_POINT('',(9.5,-8.25,-7.93856620135736));
#37048=CARTESIAN_POINT('Origin',(9.75,-10.75,3.17542648054294));
#37049=CARTESIAN_POINT('',(10.,-10.5,3.17542648054294));
#37050=CARTESIAN_POINT('',(9.5,-11.,3.17542648054294));
#37051=CARTESIAN_POINT('Origin',(2.,7.77755175064932E-16,12.7017059221718));
#37052=CARTESIAN_POINT('',(2.,-2.75,11.1139926819003));
#37053=CARTESIAN_POINT('Origin',(2.,11.,6.35085296108588));
#37054=CARTESIAN_POINT('',(2.,8.25,7.93856620135735));
#37055=CARTESIAN_POINT('Origin',(2.,11.,-6.35085296108589));
#37056=CARTESIAN_POINT('',(2.,11.,-3.17542648054295));
#37057=CARTESIAN_POINT('Origin',(10.,0.,0.));
#37058=CARTESIAN_POINT('',(10.,4.5,2.59807621135332));
#37059=CARTESIAN_POINT('',(10.,0.,5.19615242270663));
#37060=CARTESIAN_POINT('',(10.,1.25,4.4744645862196));
#37061=CARTESIAN_POINT('',(10.,4.5,-2.59807621135332));
#37062=CARTESIAN_POINT('',(10.,4.5,1.15470053837925));
#37063=CARTESIAN_POINT('',(10.,-5.55111512312578E-16,-5.19615242270663));
#37064=CARTESIAN_POINT('',(10.,3.25,-3.31976404784035));
#37065=CARTESIAN_POINT('',(10.,-4.5,-2.59807621135332));
#37066=CARTESIAN_POINT('',(10.,-1.25,-4.4744645862196));
#37067=CARTESIAN_POINT('',(10.,-4.5,2.59807621135332));
#37068=CARTESIAN_POINT('',(10.,-4.5,-1.15470053837925));
#37069=CARTESIAN_POINT('',(10.,-3.25,3.31976404784035));
#37070=CARTESIAN_POINT('Origin',(9.75,-1.125,-4.25795823527349));
#37071=CARTESIAN_POINT('',(9.5,-8.48460190979926E-16,-4.61880215351701));
#37072=CARTESIAN_POINT('',(10.,-1.11022302462516E-15,-5.19615242270663));
#37073=CARTESIAN_POINT('',(9.5,-4.,-2.3094010767585));
#37074=CARTESIAN_POINT('',(9.5,-1.,-4.04145188432738));
#37075=CARTESIAN_POINT('',(10.,-4.5,-2.59807621135332));
#37076=CARTESIAN_POINT('Origin',(9.75,3.125,-3.10325769689424));
#37077=CARTESIAN_POINT('',(9.5,4.,-2.30940107675851));
#37078=CARTESIAN_POINT('',(10.,4.5,-2.59807621135332));
#37079=CARTESIAN_POINT('',(9.5,3.,-2.88675134594813));
#37080=CARTESIAN_POINT('Origin',(9.75,1.125,4.25795823527349));
#37081=CARTESIAN_POINT('',(9.5,2.82820063659975E-16,4.61880215351701));
#37082=CARTESIAN_POINT('',(10.,0.,5.19615242270663));
#37083=CARTESIAN_POINT('',(9.5,4.,2.3094010767585));
#37084=CARTESIAN_POINT('',(9.5,1.,4.04145188432738));
#37085=CARTESIAN_POINT('',(9.5,4.,2.3094010767585));
#37086=CARTESIAN_POINT('Origin',(9.75,-3.125,3.10325769689424));
#37087=CARTESIAN_POINT('',(9.5,-4.,2.3094010767585));
#37088=CARTESIAN_POINT('',(9.5,-3.,2.88675134594813));
#37089=CARTESIAN_POINT('',(10.,-4.5,2.59807621135332));
#37090=CARTESIAN_POINT('Origin',(9.75,4.25,1.15470053837925));
#37091=CARTESIAN_POINT('',(9.5,4.,1.15470053837925));
#37092=CARTESIAN_POINT('Origin',(9.75,-4.25,-1.15470053837925));
#37093=CARTESIAN_POINT('',(9.5,-4.,-1.15470053837925));
#37094=CARTESIAN_POINT('Origin',(10.,4.,-2.30940107675851));
#37095=CARTESIAN_POINT('',(5.,4.,-2.30940107675851));
#37096=CARTESIAN_POINT('',(10.,4.,-2.30940107675851));
#37097=CARTESIAN_POINT('',(5.,-1.11022302462516E-15,-4.61880215351701));
#37098=CARTESIAN_POINT('',(5.,-8.48460190979926E-16,-4.61880215351701));
#37099=CARTESIAN_POINT('',(10.,-8.48460190979926E-16,-4.61880215351701));
#37100=CARTESIAN_POINT('Origin',(10.,4.,2.3094010767585));
#37101=CARTESIAN_POINT('',(5.,4.,2.3094010767585));
#37102=CARTESIAN_POINT('',(10.,4.,2.3094010767585));
#37103=CARTESIAN_POINT('',(5.,4.,-2.30940107675851));
#37104=CARTESIAN_POINT('Origin',(10.,5.55111512312578E-16,4.61880215351701));
#37105=CARTESIAN_POINT('',(5.,5.55111512312578E-16,4.61880215351701));
#37106=CARTESIAN_POINT('',(10.,2.82820063659975E-16,4.61880215351701));
#37107=CARTESIAN_POINT('',(5.,4.,2.3094010767585));
#37108=CARTESIAN_POINT('Ctrl Pts',(-12.0695005055609,-3.51734582803218,
7.26147165359919));
#37109=CARTESIAN_POINT('Ctrl Pts',(-12.0303542073922,-4.70805021950285,
6.68471265438406));
#37110=CARTESIAN_POINT('Ctrl Pts',(-11.9520616110547,-6.79926924260069,
4.93500196856942));
#37111=CARTESIAN_POINT('Ctrl Pts',(-11.8346227165485,-8.32382364819228,
1.13769958140006));
#37112=CARTESIAN_POINT('Ctrl Pts',(-11.7171838220422,-7.87424867921618,
-2.928432376846));
#37113=CARTESIAN_POINT('Ctrl Pts',(-11.599744927536,-5.55735101149824,-6.30056026334087));
#37114=CARTESIAN_POINT('Ctrl Pts',(-11.4823060330297,-1.92248730937921,
-8.17826163021399));
#37115=CARTESIAN_POINT('Ctrl Pts',(-11.3648671385235,2.16827971646752,-8.11660023363346));
#37116=CARTESIAN_POINT('Ctrl Pts',(-11.2474282440173,5.74484511045451,-6.13001490910025));
#37117=CARTESIAN_POINT('Ctrl Pts',(-11.129989349511,7.95900894851219,-2.68972043029039));
#37118=CARTESIAN_POINT('Ctrl Pts',(-11.0125504550048,8.28568610932253,1.38846061981056));
#37119=CARTESIAN_POINT('Ctrl Pts',(-10.8951115604986,6.64740134656684,5.1373583652959));
#37120=CARTESIAN_POINT('Ctrl Pts',(-10.7776726659924,3.43267763704583,7.66792930081125));
#37121=CARTESIAN_POINT('Ctrl Pts',(-10.6602337714861,-0.596110146715297,
8.38003913890674));
#37122=CARTESIAN_POINT('Ctrl Pts',(-10.5427948769799,-4.48352951771318,
7.10481331033355));
#37123=CARTESIAN_POINT('Ctrl Pts',(-10.4253559824737,-7.3076743467974,4.14467160188776));
#37124=CARTESIAN_POINT('Ctrl Pts',(-10.3079170879674,-8.3987950520306,0.201616129083312));
#37125=CARTESIAN_POINT('Ctrl Pts',(-10.1904781934612,-7.4981310548925,-3.78925300008877));
#37126=CARTESIAN_POINT('Ctrl Pts',(-10.073039298955,-4.81927591637304,-6.88149598316814));
#37127=CARTESIAN_POINT('Ctrl Pts',(-9.95560040444872,-0.997523488572918,
-8.34178364717233));
#37128=CARTESIAN_POINT('Ctrl Pts',(-9.83816150994251,3.06079288122268,-7.82380689682625));
#37129=CARTESIAN_POINT('Ctrl Pts',(-9.72072261543626,6.39323840044666,-5.45040459216995));
#37130=CARTESIAN_POINT('Ctrl Pts',(-9.60328372093004,8.20951945985529,-1.78443203586594));
#37131=CARTESIAN_POINT('Ctrl Pts',(-9.48584482642378,8.07890273990855,2.30472080092658));
#37132=CARTESIAN_POINT('Ctrl Pts',(-9.36840593191757,6.03236415915333,5.84730622649608));
#37133=CARTESIAN_POINT('Ctrl Pts',(-9.25096703741134,2.55524289425404,8.00319568692536));
#37134=CARTESIAN_POINT('Ctrl Pts',(-9.1335281429051,-1.5278574099364,8.26111730873075));
#37135=CARTESIAN_POINT('Ctrl Pts',(-9.01608924839887,-5.24862442380086,
6.55990465713925));
#37136=CARTESIAN_POINT('Ctrl Pts',(-8.89865035389263,-7.7246736093346,3.30300243451213));
#37137=CARTESIAN_POINT('Ctrl Pts',(-8.78121145938641,-8.36880681401512,
-0.737210935087755));
#37138=CARTESIAN_POINT('Ctrl Pts',(-8.66377256488016,-7.02826704496481,
-4.60259381194273));
#37139=CARTESIAN_POINT('Ctrl Pts',(-8.54633367037395,-4.02096498037294,
-7.37646582583656));
#37140=CARTESIAN_POINT('Ctrl Pts',(-8.4288947758677,-0.0600860556372529,
-8.400999769016));
#37141=CARTESIAN_POINT('Ctrl Pts',(-8.31145588136148,3.91504235213327,-7.43322613904));
#37142=CARTESIAN_POINT('Ctrl Pts',(-8.19401698685524,6.96171358315727,-4.70265365928452));
#37143=CARTESIAN_POINT('Ctrl Pts',(-8.07657809234901,8.35740575511295,-0.856840998963709));
#37144=CARTESIAN_POINT('Ctrl Pts',(-7.95913919784278,7.77112872867905,3.19217257293514));
#37145=CARTESIAN_POINT('Ctrl Pts',(-7.84170030333654,5.34191883189369,6.48415843780511));
#37146=CARTESIAN_POINT('Ctrl Pts',(-7.72426140883031,1.64586622155058,8.23841804194586));
#37147=CARTESIAN_POINT('Ctrl Pts',(-7.60682251432408,-2.44050561599858,
8.038926532279));
#37148=CARTESIAN_POINT('Ctrl Pts',(-7.48938361981785,-5.94810850285432,
5.93299356913289));
#37149=CARTESIAN_POINT('Ctrl Pts',(-7.37194472531161,-8.04511003962913,
2.42004378128959));
#37150=CARTESIAN_POINT('Ctrl Pts',(-7.25450583080538,-8.23420369644436,
-1.66682240762538));
#37151=CARTESIAN_POINT('Ctrl Pts',(-7.13706693629915,-6.47054567674393,
-5.35839958366958));
#37152=CARTESIAN_POINT('Ctrl Pts',(-7.01962804179292,-3.17238967957803,
-7.77922561531716));
#37153=CARTESIAN_POINT('Ctrl Pts',(-6.90218914728668,0.878102486783198,
-8.35519858984843));
#37154=CARTESIAN_POINT('Ctrl Pts',(-6.78475025278046,4.72035155321251,-6.94972579798543));
#37155=CARTESIAN_POINT('Ctrl Pts',(-6.66731135827422,7.4431633614575,-3.89611686525913));
#37156=CARTESIAN_POINT('Ctrl Pts',(-6.54987246376799,8.40081969523418,0.0814610413973314));
#37157=CARTESIAN_POINT('Ctrl Pts',(-6.43243356926176,7.36621116057458,4.03972036048615));
#37158=CARTESIAN_POINT('Ctrl Pts',(-6.31499467475553,4.58469646186278,7.03995495764589));
#37159=CARTESIAN_POINT('Ctrl Pts',(-6.1975557802493,0.715915279072651,8.3706554561928));
#37160=CARTESIAN_POINT('Ctrl Pts',(-6.08011688574306,-3.32264610505695,
7.71624457321371));
#37161=CARTESIAN_POINT('Ctrl Pts',(-5.96267799123684,-6.57323782128532,
5.23191666580462));
#37162=CARTESIAN_POINT('Ctrl Pts',(-5.84523909673059,-8.26497798989004,
1.50683319572324));
#37163=CARTESIAN_POINT('Ctrl Pts',(-5.72780020222437,-7.99666831990594,
-2.5755976460838));
#37164=CARTESIAN_POINT('Ctrl Pts',(-5.61036130771812,-5.83193878421242,
-6.0472222937725));
#37165=CARTESIAN_POINT('Ctrl Pts',(-5.49292241321191,-2.28415769210351,
-8.08474063224692));
#37166=CARTESIAN_POINT('Ctrl Pts',(-5.37548351870566,1.80531424554574,-8.20495264629408));
#37167=CARTESIAN_POINT('Ctrl Pts',(-5.25804462419944,5.46665365823166,-6.37934990685156));
#37168=CARTESIAN_POINT('Ctrl Pts',(-5.14060572969319,7.83156933772,-3.0408763805148));
#37169=CARTESIAN_POINT('Ctrl Pts',(-5.02316683518698,8.3392185810425,1.01874477211711));
#37170=CARTESIAN_POINT('Ctrl Pts',(-4.90572794068073,6.86921173698437,4.83676933143891));
#37171=CARTESIAN_POINT('Ctrl Pts',(-4.78828904617451,3.770162762059,7.50774801126825));
#37172=CARTESIAN_POINT('Ctrl Pts',(-4.67085015166827,-0.222985014150146,
8.39825488638014));
#37173=CARTESIAN_POINT('Ctrl Pts',(-4.55341125716204,-4.16325161610056,
7.29710514066449));
#37174=CARTESIAN_POINT('Ctrl Pts',(-4.43597236265581,-7.1161979048615,4.46543780972854));
#37175=CARTESIAN_POINT('Ctrl Pts',(-4.31853346814957,-8.3815289848282,0.574786332771845));
#37176=CARTESIAN_POINT('Ctrl Pts',(-4.20109457364334,-7.65917001270053,
-3.4521764398139));
#37177=CARTESIAN_POINT('Ctrl Pts',(-4.08365567913712,-5.12042931874465,
-6.66045126420618));
#37178=CARTESIAN_POINT('Ctrl Pts',(-3.96621678463087,-1.36737242671985,
-8.28919176391845));
#37179=CARTESIAN_POINT('Ctrl Pts',(-3.84877789012465,2.70995854408127,-7.9521400989076));
#37180=CARTESIAN_POINT('Ctrl Pts',(-3.73133899561841,6.14461946158279,-5.72922849019895));
#37181=CARTESIAN_POINT('Ctrl Pts',(-3.61390010111218,8.12207621918668,-2.14762320163677));
#37182=CARTESIAN_POINT('Ctrl Pts',(-3.49646120660595,8.17337245336549,1.94329361215914));
#37183=CARTESIAN_POINT('Ctrl Pts',(-3.37902231209972,6.28634325160488,5.57335591345347));
#37184=CARTESIAN_POINT('Ctrl Pts',(-3.26158341759348,2.90849983754228,7.88168992567818));
#37185=CARTESIAN_POINT('Ctrl Pts',(-3.14414452308725,-1.1590978033505,8.32087130825875));
#37186=CARTESIAN_POINT('Ctrl Pts',(-3.02670562858102,-4.95181422457809,
6.78674774808702));
#37187=CARTESIAN_POINT('Ctrl Pts',(-2.90926673407478,-7.57020119484931,
3.64313836494415));
#37188=CARTESIAN_POINT('Ctrl Pts',(-2.79182783956855,-8.39330655635519,
-0.364445569542508));
#37189=CARTESIAN_POINT('Ctrl Pts',(-2.67438894506232,-7.2259267400895,-4.28560128601273));
#37190=CARTESIAN_POINT('Ctrl Pts',(-2.55695005055609,-4.34491343911961,
-7.1904203216184));
#37191=CARTESIAN_POINT('Ctrl Pts',(-2.43951115604986,-0.433490517027392,
-8.39002416011216));
#37192=CARTESIAN_POINT('Ctrl Pts',(-2.32207226154363,3.58071951422406,-7.59991946597854));
#37193=CARTESIAN_POINT('Ctrl Pts',(-2.20463336703739,6.74578836548944,-5.00749194802054));
#37194=CARTESIAN_POINT('Ctrl Pts',(-2.08719447253116,8.31102423036551,-1.22751659427962));
#37195=CARTESIAN_POINT('Ctrl Pts',(-1.96975557802493,7.90541015591722,2.84353655923596));
#37196=CARTESIAN_POINT('Ctrl Pts',(-1.8523166835187,5.62478208560713,6.24029926664823));
#37197=CARTESIAN_POINT('Ctrl Pts',(-1.73487778901246,2.01069766784778,8.15705187872645));
#37198=CARTESIAN_POINT('Ctrl Pts',(-1.61743889450623,-2.08118048114745,
8.1395942446814));
#37199=CARTESIAN_POINT('Ctrl Pts',(-1.53914629816874,-4.4785344754388,6.8406029773222));
#37200=CARTESIAN_POINT('Ctrl Pts',(-1.5,-5.45359047959038,5.94634704090849));
#37201=CARTESIAN_POINT('Ctrl Pts',(-11.9046670037073,-3.64180542199675,
7.5184153428974));
#37202=CARTESIAN_POINT('Ctrl Pts',(-11.8655207055385,-4.87464231687759,
6.92124800331219));
#37203=CARTESIAN_POINT('Ctrl Pts',(-11.7872281092011,-7.03985812142109,
5.10962464465874));
#37204=CARTESIAN_POINT('Ctrl Pts',(-11.6697892146948,-8.61835815294024,
1.17795653504568));
#37205=CARTESIAN_POINT('Ctrl Pts',(-11.5523503201886,-8.15287518946173,
-3.03205355099106));
#37206=CARTESIAN_POINT('Ctrl Pts',(-11.4349114256823,-5.75399520977336,
-6.52350256428699));
#37207=CARTESIAN_POINT('Ctrl Pts',(-11.3174725311761,-1.99051360011823,
-8.4676454928187));
#37208=CARTESIAN_POINT('Ctrl Pts',(-11.2000336366699,2.24500325356257,-8.40380223731473));
#37209=CARTESIAN_POINT('Ctrl Pts',(-11.0825947421636,5.94812369743286,-6.34692254454031));
#37210=CARTESIAN_POINT('Ctrl Pts',(-10.9651558476574,8.24063466020584,-2.78489489677709));
#37211=CARTESIAN_POINT('Ctrl Pts',(-10.8477169531512,8.5788711355618,1.43759063244685));
#37212=CARTESIAN_POINT('Ctrl Pts',(-10.7302780586449,6.88261645277555,5.31914132536183));
#37213=CARTESIAN_POINT('Ctrl Pts',(-10.6128391641387,3.5541412877091,7.93925529887552));
#37214=CARTESIAN_POINT('Ctrl Pts',(-10.4954002696325,-0.617203218152013,
8.67656280181284));
#37215=CARTESIAN_POINT('Ctrl Pts',(-10.3779613751263,-4.64217705781445,
7.35621371934393));
#37216=CARTESIAN_POINT('Ctrl Pts',(-10.26052248062,-7.56625289621931,4.2913288172734));
#37217=CARTESIAN_POINT('Ctrl Pts',(-10.1430835861138,-8.69598238392063,
0.208750219044679));
#37218=CARTESIAN_POINT('Ctrl Pts',(-10.0256446916076,-7.76344882352011,
-3.92333389883392));
#37219=CARTESIAN_POINT('Ctrl Pts',(-9.90820579710132,-4.98980368164843,
-7.12499441573858));
#37220=CARTESIAN_POINT('Ctrl Pts',(-9.79076690259509,-1.03282037845178,
-8.63695365786423));
#37221=CARTESIAN_POINT('Ctrl Pts',(-9.67332800808886,3.1690975682883,-8.10064854881163));
#37222=CARTESIAN_POINT('Ctrl Pts',(-9.55588911358262,6.61946007279314,-5.64326454272637));
#37223=CARTESIAN_POINT('Ctrl Pts',(-9.4384502190764,8.50000936575956,-1.84757330701173));
#37224=CARTESIAN_POINT('Ctrl Pts',(-9.32101132457016,8.36477083586739,2.38627224030993));
#37225=CARTESIAN_POINT('Ctrl Pts',(-9.20357243006393,6.24581646967428,6.05421035088903));
#37226=CARTESIAN_POINT('Ctrl Pts',(-9.08613353555769,2.64565893767098,8.28638492515022));
#37227=CARTESIAN_POINT('Ctrl Pts',(-8.96869464105146,-1.58191991108739,
8.55343297975294));
#37228=CARTESIAN_POINT('Ctrl Pts',(-8.85125574654523,-5.43434447994452,
6.79202373498684));
#37229=CARTESIAN_POINT('Ctrl Pts',(-8.73381685203899,-7.99800747752137,
3.41987759037174));
#37230=CARTESIAN_POINT('Ctrl Pts',(-8.61637795753277,-8.66493302649592,
-0.763296790199302));
#37231=CARTESIAN_POINT('Ctrl Pts',(-8.49893906302653,-7.27695890111372,
-4.76545438495005));
#37232=CARTESIAN_POINT('Ctrl Pts',(-8.38150016852031,-4.16324489632963,
-7.6374785287276));
#37233=CARTESIAN_POINT('Ctrl Pts',(-8.26406127401406,-0.0622121718775053,
-8.6982651137584));
#37234=CARTESIAN_POINT('Ctrl Pts',(-8.14662237950784,4.05357424672756,-7.69624727837146));
#37235=CARTESIAN_POINT('Ctrl Pts',(-8.0291834850016,7.20805047700265,-4.86905480196603));
#37236=CARTESIAN_POINT('Ctrl Pts',(-7.91174459049537,8.65312854659645,-0.887159906468719));
#37237=CARTESIAN_POINT('Ctrl Pts',(-7.79430569598914,8.04610638896758,3.30512606733595));
#37238=CARTESIAN_POINT('Ctrl Pts',(-7.6768668014829,5.53094006589079,6.71359727203618));
#37239=CARTESIAN_POINT('Ctrl Pts',(-7.55942790697667,1.70410440786188,8.52993051030745));
#37240=CARTESIAN_POINT('Ctrl Pts',(-7.44198901247044,-2.52686173589292,
8.32338008931757));
#37241=CARTESIAN_POINT('Ctrl Pts',(-7.32455011796421,-6.15857946741587,
6.14292969901917));
#37242=CARTESIAN_POINT('Ctrl Pts',(-7.20711122345797,-8.32978239710749,
2.5056758689835));
#37243=CARTESIAN_POINT('Ctrl Pts',(-7.08967232895176,-8.52556704221308,
-1.72580211852295));
#37244=CARTESIAN_POINT('Ctrl Pts',(-6.9722334344455,-6.69950282995833,-5.54800398115828));
#37245=CARTESIAN_POINT('Ctrl Pts',(-6.85479453993929,-3.28464316579227,
-8.05448978005325));
#37246=CARTESIAN_POINT('Ctrl Pts',(-6.73735564543304,0.909173721830177,
-8.65084328184839));
#37247=CARTESIAN_POINT('Ctrl Pts',(-6.61991675092682,4.8873789273765,-7.19563850980607));
#37248=CARTESIAN_POINT('Ctrl Pts',(-6.50247785642058,7.7065361246348,-4.03397909058373));
#37249=CARTESIAN_POINT('Ctrl Pts',(-6.38503896191435,8.69807866815224,0.084343501249706));
#37250=CARTESIAN_POINT('Ctrl Pts',(-6.26760006740812,7.62686100705708,4.18266392656644));
#37251=CARTESIAN_POINT('Ctrl Pts',(-6.15016117290189,4.74692374572742,7.28906038497536));
#37252=CARTESIAN_POINT('Ctrl Pts',(-6.03272227839565,0.741247597617024,
8.6668470819898));
#37253=CARTESIAN_POINT('Ctrl Pts',(-5.91528338388943,-3.44021634277074,
7.98928018400289));
#37254=CARTESIAN_POINT('Ctrl Pts',(-5.79784448938318,-6.80582868674692,
5.41704552595052));
#37255=CARTESIAN_POINT('Ctrl Pts',(-5.68040559487697,-8.55743026926212,
1.56015176514495));
#37256=CARTESIAN_POINT('Ctrl Pts',(-5.56296670037072,-8.27962659038162,
-2.6667339326249));
#37257=CARTESIAN_POINT('Ctrl Pts',(-5.4455278058645,-6.03829913903584,-6.26120035225574));
#37258=CARTESIAN_POINT('Ctrl Pts',(-5.32808891135826,-2.36498151575047,
-8.37081529922423));
#37259=CARTESIAN_POINT('Ctrl Pts',(-5.21065001685203,1.86919442365855,-8.49528095769237));
#37260=CARTESIAN_POINT('Ctrl Pts',(-5.0932111223458,5.66008857419189,-6.60508014151799));
#37261=CARTESIAN_POINT('Ctrl Pts',(-4.97577222783956,8.10868565995078,-3.14847633176188));
#37262=CARTESIAN_POINT('Ctrl Pts',(-4.85833333333333,8.63429782810052,1.05479256692895));
#37263=CARTESIAN_POINT('Ctrl Pts',(-4.7408944388271,7.11227549739945,5.00791609281038));
#37264=CARTESIAN_POINT('Ctrl Pts',(-4.62345554432086,3.9035681618939,7.77340607128152));
#37265=CARTESIAN_POINT('Ctrl Pts',(-4.50601664981463,-0.230875231853538,
8.6954231047679));
#37266=CARTESIAN_POINT('Ctrl Pts',(-4.3885777553084,-4.31056627637157,7.5553097038001));
#37267=CARTESIAN_POINT('Ctrl Pts',(-4.27113886080217,-7.36800115228518,
4.62344518342595));
#37268=CARTESIAN_POINT('Ctrl Pts',(-4.15369996629594,-8.67810536521717,
0.595124871286611));
#37269=CARTESIAN_POINT('Ctrl Pts',(-4.0362610717897,-7.93018606755907,-3.57433004625461));
#37270=CARTESIAN_POINT('Ctrl Pts',(-3.91882217728347,-5.30161325262351,
-6.89612813548719));
#37271=CARTESIAN_POINT('Ctrl Pts',(-3.80138328277724,-1.41575624376498,
-8.58250083606305));
#37272=CARTESIAN_POINT('Ctrl Pts',(-3.683944388271,2.80584912651111,-8.23352275965472));
#37273=CARTESIAN_POINT('Ctrl Pts',(-3.56650549376478,6.36204387210294,-5.93195449056479));
#37274=CARTESIAN_POINT('Ctrl Pts',(-3.44906659925854,8.40947198798854,-2.2236158178687));
#37275=CARTESIAN_POINT('Ctrl Pts',(-3.33162770475231,8.46258331479401,2.01205612393598));
#37276=CARTESIAN_POINT('Ctrl Pts',(-3.21418881024607,6.50878249041422,5.77056643750267));
#37277=CARTESIAN_POINT('Ctrl Pts',(-3.09674991573985,3.01141570835078,8.16057974085834));
#37278=CARTESIAN_POINT('Ctrl Pts',(-2.97931102123361,-1.20011192280969,
8.61530134587515));
#37279=CARTESIAN_POINT('Ctrl Pts',(-2.86187212672739,-5.12703179427717,
7.0268935598338));
#37280=CARTESIAN_POINT('Ctrl Pts',(-2.74443323222114,-7.838069130789,3.77204906745287));
#37281=CARTESIAN_POINT('Ctrl Pts',(-2.62699433771492,-8.69029968045997,
-0.37734130110405));
#37282=CARTESIAN_POINT('Ctrl Pts',(-2.50955544320868,-7.48161268968305,
-4.43724523063151));
#37283=CARTESIAN_POINT('Ctrl Pts',(-2.39211654870245,-4.49865611580904,
-7.44484989363574));
#37284=CARTESIAN_POINT('Ctrl Pts',(-2.27467765419622,-0.448829370917385,
-8.68690113820128));
#37285=CARTESIAN_POINT('Ctrl Pts',(-2.15723875968999,3.70742155565816,-7.86883896867878));
#37286=CARTESIAN_POINT('Ctrl Pts',(-2.03979986518376,6.98448484914156,-5.18467964724095));
#37287=CARTESIAN_POINT('Ctrl Pts',(-1.92236097067752,8.6051058338568,-1.27095167981805));
#37288=CARTESIAN_POINT('Ctrl Pts',(-1.80492207617129,8.18513930005979,2.94415373562089));
#37289=CARTESIAN_POINT('Ctrl Pts',(-1.68748318166506,5.82381230007586,6.46110926114882));
#37290=CARTESIAN_POINT('Ctrl Pts',(-1.57004428715883,2.08184523978439,8.44568524445446));
#37291=CARTESIAN_POINT('Ctrl Pts',(-1.45260539265259,-2.15482205360423,
8.42760988040756));
#37292=CARTESIAN_POINT('Ctrl Pts',(-1.3743127963151,-4.63700526836658,7.08265443050748));
#37293=CARTESIAN_POINT('Ctrl Pts',(-1.33516649814636,-5.6465631612441,6.15675567698451));
#37294=CARTESIAN_POINT('Ctrl Pts',(-11.7398335018536,-3.76626501596132,
7.77535903219561));
#37295=CARTESIAN_POINT('Ctrl Pts',(-11.7006872036849,-5.04123441425232,
7.15778335224033));
#37296=CARTESIAN_POINT('Ctrl Pts',(-11.6223946073474,-7.2804470002415,5.28424732074805));
#37297=CARTESIAN_POINT('Ctrl Pts',(-11.5049557128412,-8.91289265768821,
1.21821348869131));
#37298=CARTESIAN_POINT('Ctrl Pts',(-11.3875168183349,-8.43150169970728,
-3.13567472513613));
#37299=CARTESIAN_POINT('Ctrl Pts',(-11.2700779238287,-5.95063940804848,
-6.74644486523312));
#37300=CARTESIAN_POINT('Ctrl Pts',(-11.1526390293225,-2.05853989085726,
-8.75702935542341));
#37301=CARTESIAN_POINT('Ctrl Pts',(-11.0352001348162,2.32172679065763,-8.69100424099601));
#37302=CARTESIAN_POINT('Ctrl Pts',(-10.91776124031,6.15140228441119,-6.56383017998038));
#37303=CARTESIAN_POINT('Ctrl Pts',(-10.8003223458038,8.5222603718995,-2.88006936326379));
#37304=CARTESIAN_POINT('Ctrl Pts',(-10.6828834512975,8.87205616180107,1.48672064508313));
#37305=CARTESIAN_POINT('Ctrl Pts',(-10.5654445567913,7.11783155898424,5.50092428542775));
#37306=CARTESIAN_POINT('Ctrl Pts',(-10.4480056622851,3.67560493837237,8.21058129693979));
#37307=CARTESIAN_POINT('Ctrl Pts',(-10.3305667677788,-0.638296289588734,
8.97308646471894));
#37308=CARTESIAN_POINT('Ctrl Pts',(-10.2131278732726,-4.80082459791572,
7.6076141283543));
#37309=CARTESIAN_POINT('Ctrl Pts',(-10.0956889787664,-7.82483144564121,
4.43798603265904));
#37310=CARTESIAN_POINT('Ctrl Pts',(-9.97825008426014,-8.99316971581067,
0.215884309006054));
#37311=CARTESIAN_POINT('Ctrl Pts',(-9.86081118975393,-8.02876659214771,
-4.05741479757908));
#37312=CARTESIAN_POINT('Ctrl Pts',(-9.74337229524768,-5.16033144692384,
-7.36849284830899));
#37313=CARTESIAN_POINT('Ctrl Pts',(-9.62593340074146,-1.06811726833064,
-8.93212366855616));
#37314=CARTESIAN_POINT('Ctrl Pts',(-9.50849450623522,3.27740225535393,-8.37749020079698));
#37315=CARTESIAN_POINT('Ctrl Pts',(-9.39105561172899,6.84568174513961,-5.8361244932828));
#37316=CARTESIAN_POINT('Ctrl Pts',(-9.27361671722275,8.79049927166384,-1.91071457815751));
#37317=CARTESIAN_POINT('Ctrl Pts',(-9.15617782271652,8.65063893182622,2.46782367969326));
#37318=CARTESIAN_POINT('Ctrl Pts',(-9.03873892821028,6.45926878019523,6.26111447528199));
#37319=CARTESIAN_POINT('Ctrl Pts',(-8.92130003370407,2.73607498108792,8.56957416337506));
#37320=CARTESIAN_POINT('Ctrl Pts',(-8.80386113919782,-1.63598241223839,
8.84574865077515));
#37321=CARTESIAN_POINT('Ctrl Pts',(-8.6864222446916,-5.62006453608818,7.02414281283443));
#37322=CARTESIAN_POINT('Ctrl Pts',(-8.56898335018536,-8.27134134570815,
3.53675274623135));
#37323=CARTESIAN_POINT('Ctrl Pts',(-8.45154445567913,-8.96105923897671,
-0.789382645310846));
#37324=CARTESIAN_POINT('Ctrl Pts',(-8.33410556117289,-7.52565075726262,
-4.92831495795738));
#37325=CARTESIAN_POINT('Ctrl Pts',(-8.21666666666667,-4.30552481228632,
-7.89849123161864));
#37326=CARTESIAN_POINT('Ctrl Pts',(-8.09922777216043,-0.0643382881177545,
-8.99553045850081));
#37327=CARTESIAN_POINT('Ctrl Pts',(-7.98178887765419,4.19210614132184,-7.95926841770293));
#37328=CARTESIAN_POINT('Ctrl Pts',(-7.86434998314797,7.45438737084802,-5.03545594464754));
#37329=CARTESIAN_POINT('Ctrl Pts',(-7.74691108864173,8.94885133807996,-0.917478813973732));
#37330=CARTESIAN_POINT('Ctrl Pts',(-7.6294721941355,8.32108404925609,3.41807956173676));
#37331=CARTESIAN_POINT('Ctrl Pts',(-7.51203329962926,5.7199612998879,6.94303610626724));
#37332=CARTESIAN_POINT('Ctrl Pts',(-7.39459440512304,1.76234259417318,8.82144297866904));
#37333=CARTESIAN_POINT('Ctrl Pts',(-7.27715551061681,-2.61321785578727,
8.60783364635613));
#37334=CARTESIAN_POINT('Ctrl Pts',(-7.15971661611056,-6.36905043197742,
6.35286582890546));
#37335=CARTESIAN_POINT('Ctrl Pts',(-7.04227772160434,-8.61445475458585,
2.59130795667739));
#37336=CARTESIAN_POINT('Ctrl Pts',(-6.92483882709811,-8.81693038798178,
-1.78478182942051));
#37337=CARTESIAN_POINT('Ctrl Pts',(-6.80739993259187,-6.92845998317274,
-5.73760837864699));
#37338=CARTESIAN_POINT('Ctrl Pts',(-6.68996103808565,-3.3968966520065,-8.32975394478933));
#37339=CARTESIAN_POINT('Ctrl Pts',(-6.5725221435794,0.940244956877155,-8.94648797384835));
#37340=CARTESIAN_POINT('Ctrl Pts',(-6.45508324907318,5.05440630154049,-7.44155122162673));
#37341=CARTESIAN_POINT('Ctrl Pts',(-6.33764435456694,7.96990888781211,-4.17184131590833));
#37342=CARTESIAN_POINT('Ctrl Pts',(-6.22020546006072,8.99533764107029,0.0872259611020821));
#37343=CARTESIAN_POINT('Ctrl Pts',(-6.10276656555447,7.88751085353959,4.32560749264671));
#37344=CARTESIAN_POINT('Ctrl Pts',(-5.98532767104826,4.90915102959206,7.53816581230484));
#37345=CARTESIAN_POINT('Ctrl Pts',(-5.86788877654201,0.766579916161399,
8.96303870778679));
#37346=CARTESIAN_POINT('Ctrl Pts',(-5.75044988203579,-3.55778658048453,
8.26231579479207));
#37347=CARTESIAN_POINT('Ctrl Pts',(-5.63301098752954,-7.03841955220852,
5.60217438609644));
#37348=CARTESIAN_POINT('Ctrl Pts',(-5.51557209302333,-8.84988254863418,
1.61347033456665));
#37349=CARTESIAN_POINT('Ctrl Pts',(-5.39813319851708,-8.56258486085733,
-2.757870219166));
#37350=CARTESIAN_POINT('Ctrl Pts',(-5.28069430401086,-6.24465949385924,
-6.47517841073899));
#37351=CARTESIAN_POINT('Ctrl Pts',(-5.16325540950462,-2.44580533939745,
-8.65688996620155));
#37352=CARTESIAN_POINT('Ctrl Pts',(-5.04581651499839,1.93307460177137,-8.78560926909064));
#37353=CARTESIAN_POINT('Ctrl Pts',(-4.92837762049216,5.85352349015212,-6.83081037618444));
#37354=CARTESIAN_POINT('Ctrl Pts',(-4.81093872598592,8.38580198218156,-3.25607628300896));
#37355=CARTESIAN_POINT('Ctrl Pts',(-4.69349983147969,8.92937707515854,1.0908403617408));
#37356=CARTESIAN_POINT('Ctrl Pts',(-4.57606093697346,7.35533925781453,5.17906285418186));
#37357=CARTESIAN_POINT('Ctrl Pts',(-4.45862204246723,4.0369735617288,8.03906413129479));
#37358=CARTESIAN_POINT('Ctrl Pts',(-4.34118314796099,-0.238765449556927,
8.99259132315565));
#37359=CARTESIAN_POINT('Ctrl Pts',(-4.22374425345476,-4.45788093664258,
7.81351426693571));
#37360=CARTESIAN_POINT('Ctrl Pts',(-4.10630535894853,-7.61980439970885,
4.78145255712337));
#37361=CARTESIAN_POINT('Ctrl Pts',(-3.98886646444229,-8.97468174560615,
0.615463409801377));
#37362=CARTESIAN_POINT('Ctrl Pts',(-3.87142756993607,-8.20120212241758,
-3.69648365269531));
#37363=CARTESIAN_POINT('Ctrl Pts',(-3.75398867542983,-5.48279718650238,
-7.1318050067682));
#37364=CARTESIAN_POINT('Ctrl Pts',(-3.6365497809236,-1.46414006081009,-8.87580990820765));
#37365=CARTESIAN_POINT('Ctrl Pts',(-3.51911088641737,2.90173970894095,-8.51490542040183));
#37366=CARTESIAN_POINT('Ctrl Pts',(-3.40167199191113,6.57946828262311,-6.13468049093065));
#37367=CARTESIAN_POINT('Ctrl Pts',(-3.28423309740491,8.69686775679039,-2.29960843410063));
#37368=CARTESIAN_POINT('Ctrl Pts',(-3.16679420289867,8.7517941762225,2.0808186357128));
#37369=CARTESIAN_POINT('Ctrl Pts',(-3.04935530839244,6.73122172922358,5.96777696155187));
#37370=CARTESIAN_POINT('Ctrl Pts',(-2.93191641388621,3.11433157915927,8.43946955603849));
#37371=CARTESIAN_POINT('Ctrl Pts',(-2.81447751937998,-1.24112604226888,
8.90973138349155));
#37372=CARTESIAN_POINT('Ctrl Pts',(-2.69703862487374,-5.30224936397625,
7.26703937158057));
#37373=CARTESIAN_POINT('Ctrl Pts',(-2.57959973036751,-8.1059370667287,3.9009597699616));
#37374=CARTESIAN_POINT('Ctrl Pts',(-2.46216083586128,-8.98729280456475,
-0.390237032665602));
#37375=CARTESIAN_POINT('Ctrl Pts',(-2.34472194135504,-7.7372986392766,-4.58888917525028));
#37376=CARTESIAN_POINT('Ctrl Pts',(-2.22728304684881,-4.65239879249847,
-7.69927946565311));
#37377=CARTESIAN_POINT('Ctrl Pts',(-2.10984415234258,-0.46416822480737,
-8.98377811629039));
#37378=CARTESIAN_POINT('Ctrl Pts',(-1.99240525783635,3.83412359709224,-8.13775847137902));
#37379=CARTESIAN_POINT('Ctrl Pts',(-1.87496636333012,7.22318133279369,-5.36186734646136));
#37380=CARTESIAN_POINT('Ctrl Pts',(-1.75752746882388,8.89918743734806,-1.31438676535649));
#37381=CARTESIAN_POINT('Ctrl Pts',(-1.64008857431765,8.46486844420237,3.04477091200582));
#37382=CARTESIAN_POINT('Ctrl Pts',(-1.52264967981142,6.02284251454457,6.68191925564942));
#37383=CARTESIAN_POINT('Ctrl Pts',(-1.40521078530519,2.15299281172101,8.73431861018245));
#37384=CARTESIAN_POINT('Ctrl Pts',(-1.28777189079896,-2.22846362606102,
8.71562551613373));
#37385=CARTESIAN_POINT('Ctrl Pts',(-1.20947929446147,-4.79547606129435,
7.32470588369278));
#37386=CARTESIAN_POINT('Ctrl Pts',(-1.17033299629272,-5.83953584289782,
6.36716431306054));
#37387=CARTESIAN_POINT('Ctrl Pts',(-11.575,-3.8907246099259,8.03230272149382));
#37388=CARTESIAN_POINT('Ctrl Pts',(-11.5358537018313,-5.20782651162705,
7.39431870116847));
#37389=CARTESIAN_POINT('Ctrl Pts',(-11.4575611054938,-7.52103587906191,
5.45886999683736));
#37390=CARTESIAN_POINT('Ctrl Pts',(-11.3401222109875,-9.20742716243616,
1.25847044233695));
#37391=CARTESIAN_POINT('Ctrl Pts',(-11.2226833164813,-8.71012820995283,
-3.2392958992812));
#37392=CARTESIAN_POINT('Ctrl Pts',(-11.1052444219751,-6.14728360632359,
-6.96938716617923));
#37393=CARTESIAN_POINT('Ctrl Pts',(-10.9878055274688,-2.12656618159628,
-9.04641321802813));
#37394=CARTESIAN_POINT('Ctrl Pts',(-10.8703666329626,2.39845032775268,-8.97820624467727));
#37395=CARTESIAN_POINT('Ctrl Pts',(-10.7529277384564,6.35468087138952,-6.78073781542045));
#37396=CARTESIAN_POINT('Ctrl Pts',(-10.6354888439501,8.80388608359315,-2.97524382975048));
#37397=CARTESIAN_POINT('Ctrl Pts',(-10.5180499494439,9.16524118804035,1.53585065771941));
#37398=CARTESIAN_POINT('Ctrl Pts',(-10.4006110549377,7.35304666519293,5.68270724549368));
#37399=CARTESIAN_POINT('Ctrl Pts',(-10.2831721604314,3.79706858903565,8.48190729500407));
#37400=CARTESIAN_POINT('Ctrl Pts',(-10.1657332659252,-0.659389361025453,
9.26961012762504));
#37401=CARTESIAN_POINT('Ctrl Pts',(-10.048294371419,-4.95947213801698,7.85901453736469));
#37402=CARTESIAN_POINT('Ctrl Pts',(-9.93085547691273,-8.08340999506311,
4.58464324804467));
#37403=CARTESIAN_POINT('Ctrl Pts',(-9.81341658240652,-9.2903570477007,0.22301839896743));
#37404=CARTESIAN_POINT('Ctrl Pts',(-9.69597768790027,-8.29408436077532,
-4.19149569632424));
#37405=CARTESIAN_POINT('Ctrl Pts',(-9.57853879339405,-5.33085921219923,
-7.61199128087941));
#37406=CARTESIAN_POINT('Ctrl Pts',(-9.4610998988878,-1.10341415820951,-9.22729367924807));
#37407=CARTESIAN_POINT('Ctrl Pts',(-9.34366100438159,3.38570694241956,-8.65433185278234));
#37408=CARTESIAN_POINT('Ctrl Pts',(-9.22622210987534,7.07190341748608,-6.02898444383924));
#37409=CARTESIAN_POINT('Ctrl Pts',(-9.10878321536913,9.08098917756812,-1.9738558493033));
#37410=CARTESIAN_POINT('Ctrl Pts',(-8.99134432086287,8.93650702778507,2.5493751190766));
#37411=CARTESIAN_POINT('Ctrl Pts',(-8.87390542635666,6.67272109071619,6.46801859967495));
#37412=CARTESIAN_POINT('Ctrl Pts',(-8.75646653185042,2.82649102450486,8.8527634015999));
#37413=CARTESIAN_POINT('Ctrl Pts',(-8.63902763734418,-1.69004491338938,
9.13806432179736));
#37414=CARTESIAN_POINT('Ctrl Pts',(-8.52158874283796,-5.80578459223184,
7.25626189068202));
#37415=CARTESIAN_POINT('Ctrl Pts',(-8.40414984833171,-8.54467521389493,
3.65362790209096));
#37416=CARTESIAN_POINT('Ctrl Pts',(-8.28671095382549,-9.25718545145751,
-0.815468500422392));
#37417=CARTESIAN_POINT('Ctrl Pts',(-8.16927205931925,-7.77434261341153,
-5.09117553096471));
#37418=CARTESIAN_POINT('Ctrl Pts',(-8.05183316481303,-4.447804728243,-8.15950393450966));
#37419=CARTESIAN_POINT('Ctrl Pts',(-7.93439427030679,-0.0664644043580101,
-9.29279580324321));
#37420=CARTESIAN_POINT('Ctrl Pts',(-7.81695537580056,4.33063803591613,-8.22228955703439));
#37421=CARTESIAN_POINT('Ctrl Pts',(-7.69951648129433,7.70072426469339,-5.20185708732905));
#37422=CARTESIAN_POINT('Ctrl Pts',(-7.58207758678809,9.24457412956349,-0.947797721478743));
#37423=CARTESIAN_POINT('Ctrl Pts',(-7.46463869228187,8.59606170954461,3.53103305613757));
#37424=CARTESIAN_POINT('Ctrl Pts',(-7.34719979777562,5.90898253388501,7.1724749404983));
#37425=CARTESIAN_POINT('Ctrl Pts',(-7.2297609032694,1.82058078048448,9.11295544703064));
#37426=CARTESIAN_POINT('Ctrl Pts',(-7.11232200876316,-2.69957397568162,
8.8922872033947));
#37427=CARTESIAN_POINT('Ctrl Pts',(-6.99488311425694,-6.57952139653898,
6.56280195879174));
#37428=CARTESIAN_POINT('Ctrl Pts',(-6.8774442197507,-8.89912711206419,2.67694004437129));
#37429=CARTESIAN_POINT('Ctrl Pts',(-6.76000532524447,-9.10829373375051,
-1.84376154031808));
#37430=CARTESIAN_POINT('Ctrl Pts',(-6.64256643073823,-7.15741713638714,
-5.9272127761357));
#37431=CARTESIAN_POINT('Ctrl Pts',(-6.52512753623201,-3.50915013822074,
-8.60501810952541));
#37432=CARTESIAN_POINT('Ctrl Pts',(-6.40768864172577,0.971316191924136,
-9.24213266584832));
#37433=CARTESIAN_POINT('Ctrl Pts',(-6.29024974721955,5.22143367570448,-7.68746393344737));
#37434=CARTESIAN_POINT('Ctrl Pts',(-6.1728108527133,8.23328165098941,-4.30970354123293));
#37435=CARTESIAN_POINT('Ctrl Pts',(-6.05537195820708,9.29259661398837,0.0901084209544563));
#37436=CARTESIAN_POINT('Ctrl Pts',(-5.93793306370083,8.14816070002208,4.468551058727));
#37437=CARTESIAN_POINT('Ctrl Pts',(-5.82049416919461,5.07137831345671,7.78727123963432));
#37438=CARTESIAN_POINT('Ctrl Pts',(-5.70305527468838,0.791912234705773,
9.25923033358377));
#37439=CARTESIAN_POINT('Ctrl Pts',(-5.58561638018215,-3.67535681819832,
8.53535140558126));
#37440=CARTESIAN_POINT('Ctrl Pts',(-5.46817748567591,-7.27101041767012,
5.78730324624234));
#37441=CARTESIAN_POINT('Ctrl Pts',(-5.35073859116969,-9.14233482800627,
1.66678890398835));
#37442=CARTESIAN_POINT('Ctrl Pts',(-5.23329969666344,-8.84554313133302,
-2.8490065057071));
#37443=CARTESIAN_POINT('Ctrl Pts',(-5.11586080215722,-6.45101984868266,
-6.68915646922223));
#37444=CARTESIAN_POINT('Ctrl Pts',(-4.99842190765098,-2.52662916304442,
-8.94296463317886));
#37445=CARTESIAN_POINT('Ctrl Pts',(-4.88098301314475,1.99695477988418,-9.07593758048892));
#37446=CARTESIAN_POINT('Ctrl Pts',(-4.76354411863852,6.04695840611235,-7.05654061085087));
#37447=CARTESIAN_POINT('Ctrl Pts',(-4.64610522413228,8.66291830441234,-3.36367623425603));
#37448=CARTESIAN_POINT('Ctrl Pts',(-4.52866632962606,9.22445632221657,1.12688815655265));
#37449=CARTESIAN_POINT('Ctrl Pts',(-4.41122743511982,7.5984030182296,5.35020961555334));
#37450=CARTESIAN_POINT('Ctrl Pts',(-4.29378854061359,4.1703789615637,8.30472219130806));
#37451=CARTESIAN_POINT('Ctrl Pts',(-4.17634964610736,-0.246655667260323,
9.28975954154339));
#37452=CARTESIAN_POINT('Ctrl Pts',(-4.05891075160113,-4.60519559691359,
8.07171883007134));
#37453=CARTESIAN_POINT('Ctrl Pts',(-3.94147185709489,-7.87160764713254,
4.93945993082077));
#37454=CARTESIAN_POINT('Ctrl Pts',(-3.82403296258866,-9.27125812599511,
0.635801948316151));
#37455=CARTESIAN_POINT('Ctrl Pts',(-3.70659406808243,-8.47221817727612,
-3.81863725913602));
#37456=CARTESIAN_POINT('Ctrl Pts',(-3.5891551735762,-5.66398112038124,-7.36748187804921));
#37457=CARTESIAN_POINT('Ctrl Pts',(-3.47171627906996,-1.51252387785522,
-9.16911898035225));
#37458=CARTESIAN_POINT('Ctrl Pts',(-3.35427738456373,2.99763029137079,-8.79628808114895));
#37459=CARTESIAN_POINT('Ctrl Pts',(-3.23683849005749,6.79689269314325,-6.3374064912965));
#37460=CARTESIAN_POINT('Ctrl Pts',(-3.11939959555127,8.98426352559225,-2.37560105033256));
#37461=CARTESIAN_POINT('Ctrl Pts',(-3.00196070104503,9.041005037651,2.14958114748964));
#37462=CARTESIAN_POINT('Ctrl Pts',(-2.8845218065388,6.95366096803292,6.16498748560106));
#37463=CARTESIAN_POINT('Ctrl Pts',(-2.76708291203257,3.21724744996777,8.71835937121864));
#37464=CARTESIAN_POINT('Ctrl Pts',(-2.64964401752634,-1.28214016172808,
9.20416142110794));
#37465=CARTESIAN_POINT('Ctrl Pts',(-2.5322051230201,-5.47746693367532,7.50718518332735));
#37466=CARTESIAN_POINT('Ctrl Pts',(-2.41476622851387,-8.3738050026684,4.02987047247031));
#37467=CARTESIAN_POINT('Ctrl Pts',(-2.29732733400764,-9.28428592866953,
-0.403132764227142));
#37468=CARTESIAN_POINT('Ctrl Pts',(-2.17988843950141,-7.99298458887015,
-4.74053311986907));
#37469=CARTESIAN_POINT('Ctrl Pts',(-2.06244954499517,-4.8061414691879,-7.95370903767045));
#37470=CARTESIAN_POINT('Ctrl Pts',(-1.94501065048894,-0.479507078697361,
-9.28065509437951));
#37471=CARTESIAN_POINT('Ctrl Pts',(-1.82757175598271,3.96082563852633,-8.40667797407926));
#37472=CARTESIAN_POINT('Ctrl Pts',(-1.71013286147648,7.46187781644582,-5.53905504568178));
#37473=CARTESIAN_POINT('Ctrl Pts',(-1.59269396697024,9.19326904083934,-1.35782185089492));
#37474=CARTESIAN_POINT('Ctrl Pts',(-1.47525507246401,8.74459758834494,3.14538808839074));
#37475=CARTESIAN_POINT('Ctrl Pts',(-1.35781617795778,6.2218727290133,6.90272925015002));
#37476=CARTESIAN_POINT('Ctrl Pts',(-1.24037728345155,2.22414038365762,9.02295197591045));
#37477=CARTESIAN_POINT('Ctrl Pts',(-1.12293838894532,-2.3021051985178,9.0036411518599));
#37478=CARTESIAN_POINT('Ctrl Pts',(-1.04464579260783,-4.95394685422212,
7.56675733687807));
#37479=CARTESIAN_POINT('Ctrl Pts',(-1.00549949443908,-6.03250852455154,
6.57757294913656));
#37480=CARTESIAN_POINT('',(-1.5,8.66570476755281,2.13569330232889));
#37481=CARTESIAN_POINT('Ctrl Pts',(-1.5,8.66576000559871,2.13591603404143));
#37482=CARTESIAN_POINT('Ctrl Pts',(-1.5,8.60143786733659,2.35388806264619));
#37483=CARTESIAN_POINT('Ctrl Pts',(-1.5,8.52891377544564,2.56895211712534));
#37484=CARTESIAN_POINT('Ctrl Pts',(-1.5,8.4482767600922,2.78063200867923));
#37485=CARTESIAN_POINT('Ctrl Pts',(-1.5,8.41941943948704,2.85638524023751));
#37486=CARTESIAN_POINT('Ctrl Pts',(-1.5,8.38952263531352,2.93170495461832));
#37487=CARTESIAN_POINT('Ctrl Pts',(-1.5,8.3585888708654,3.00656886656796));
#37488=CARTESIAN_POINT('Ctrl Pts',(-1.5,8.27217290574518,3.2157072407433));
#37489=CARTESIAN_POINT('Ctrl Pts',(-1.5,8.17766782067611,3.42129027050491));
#37490=CARTESIAN_POINT('Ctrl Pts',(-1.5,8.07540183938106,3.62292678990022));
#37491=CARTESIAN_POINT('Ctrl Pts',(-1.5,7.97289129821306,3.82504550485008));
#37492=CARTESIAN_POINT('Ctrl Pts',(-1.5,7.86258227404303,4.0231993593376));
#37493=CARTESIAN_POINT('Ctrl Pts',(-1.5,7.74476169665056,4.216965576945));
#37494=CARTESIAN_POINT('Ctrl Pts',(-1.5,7.62760726374108,4.40963626183896));
#37495=CARTESIAN_POINT('Ctrl Pts',(-1.5,7.50302551968923,4.59796928062881));
#37496=CARTESIAN_POINT('Ctrl Pts',(-1.5,7.37126210654191,4.78151280564942));
#37497=CARTESIAN_POINT('Ctrl Pts',(-1.5,7.31559889864895,4.85905042513419));
#37498=CARTESIAN_POINT('Ctrl Pts',(-1.5,7.25865362523378,4.93573281300596));
#37499=CARTESIAN_POINT('Ctrl Pts',(-1.5,7.20044313369025,5.01152361846556));
#37500=CARTESIAN_POINT('Ctrl Pts',(-1.5,7.16709059230978,5.05494905447067));
#37501=CARTESIAN_POINT('Ctrl Pts',(-1.5,7.13332267751954,5.09808176810313));
#37502=CARTESIAN_POINT('Ctrl Pts',(-1.5,7.09914242712044,5.14091470044488));
#37503=CARTESIAN_POINT('Ctrl Pts',(-1.5,7.08237376420541,5.16192832660953));
#37504=CARTESIAN_POINT('Ctrl Pts',(-1.5,7.06550518246979,5.18287056042006));
#37505=CARTESIAN_POINT('Ctrl Pts',(-1.5,7.04854790718269,5.20372738131514));
#37506=CARTESIAN_POINT('Ctrl Pts',(-1.5,6.90705671288669,5.3777563127147));
#37507=CARTESIAN_POINT('Ctrl Pts',(-1.5,6.75922259168711,5.54605767871865));
#37508=CARTESIAN_POINT('Ctrl Pts',(-1.5,6.60536289902919,5.70825802077741));
#37509=CARTESIAN_POINT('Ctrl Pts',(-1.5,6.45204887458798,5.86988311424524));
#37510=CARTESIAN_POINT('Ctrl Pts',(-1.5,6.29275147947152,6.02545086754665));
#37511=CARTESIAN_POINT('Ctrl Pts',(-1.5,6.12774643390987,6.17455745002506));
#37512=CARTESIAN_POINT('Ctrl Pts',(-1.5,6.02442900763097,6.26792010018206));
#37513=CARTESIAN_POINT('Ctrl Pts',(-1.5,5.91887310495571,6.35874887481627));
#37514=CARTESIAN_POINT('Ctrl Pts',(-1.5,5.81113993546571,6.44693645990187));
#37515=CARTESIAN_POINT('Ctrl Pts',(-1.5,5.6382749924561,6.58843922958872));
#37516=CARTESIAN_POINT('Ctrl Pts',(-1.5,5.45980530418602,6.72314435409563));
#37517=CARTESIAN_POINT('Ctrl Pts',(-1.5,5.27618003291779,6.85081401922972));
#37518=CARTESIAN_POINT('Ctrl Pts',(-1.5,5.0936053673245,6.97775322676513));
#37519=CARTESIAN_POINT('Ctrl Pts',(-1.5,4.90593330226794,7.09773747877284));
#37520=CARTESIAN_POINT('Ctrl Pts',(-1.5,4.71358884520666,7.21048451846429));
#37521=CARTESIAN_POINT('Ctrl Pts',(-1.5,4.65195078987431,7.24661505415655));
#37522=CARTESIAN_POINT('Ctrl Pts',(-1.5,4.58983282761987,7.28200199438233));
#37523=CARTESIAN_POINT('Ctrl Pts',(-1.5,4.52724874890727,7.31663492807838));
#37524=CARTESIAN_POINT('Ctrl Pts',(-1.5,4.50584961293089,7.32847683536004));
#37525=CARTESIAN_POINT('Ctrl Pts',(-1.5,4.48439782036337,7.34022953024155));
#37526=CARTESIAN_POINT('Ctrl Pts',(-1.5,4.46290386332694,7.35188735834325));
#37527=CARTESIAN_POINT('Ctrl Pts',(-1.5,4.2684954791601,7.45732999602529));
#37528=CARTESIAN_POINT('Ctrl Pts',(-1.5,4.07041460477949,7.55514065186345));
#37529=CARTESIAN_POINT('Ctrl Pts',(-1.5,3.86912729317476,7.64515288152635));
#37530=CARTESIAN_POINT('Ctrl Pts',(-1.5,3.66778053053916,7.73519169666949));
#37531=CARTESIAN_POINT('Ctrl Pts',(-1.5,3.46322479181838,7.81742772613441));
#37532=CARTESIAN_POINT('Ctrl Pts',(-1.5,3.25590400874615,7.8916473356843));
#37533=CARTESIAN_POINT('Ctrl Pts',(-1.5,3.050998079672,7.96500244183901));
#37534=CARTESIAN_POINT('Ctrl Pts',(-1.5,2.84339051416899,8.03052693585015));
#37535=CARTESIAN_POINT('Ctrl Pts',(-1.5,2.63349743742722,8.08796583453746));
#37536=CARTESIAN_POINT('Ctrl Pts',(-1.5,2.43376039741608,8.14262545353679));
#37537=CARTESIAN_POINT('Ctrl Pts',(-1.5,2.23195315073253,8.18996285358873));
#37538=CARTESIAN_POINT('Ctrl Pts',(-1.5,2.02843125000073,8.22971455260885));
#37539=CARTESIAN_POINT('Ctrl Pts',(-1.5,1.85980622697303,8.26265022753403));
#37540=CARTESIAN_POINT('Ctrl Pts',(-1.5,1.69000390546641,8.29037758188515));
#37541=CARTESIAN_POINT('Ctrl Pts',(-1.5,1.51926769823031,8.31287539192494));
#37542=CARTESIAN_POINT('Ctrl Pts',(-1.5,1.48148098969113,8.31785452438024));
#37543=CARTESIAN_POINT('Ctrl Pts',(-1.5,1.44364855517463,8.32257743549686));
#37544=CARTESIAN_POINT('Ctrl Pts',(-1.5,1.40577306551694,8.32704377013679));
#37545=CARTESIAN_POINT('Ctrl Pts',(-1.5,1.37905825216086,8.3301940210608));
#37546=CARTESIAN_POINT('Ctrl Pts',(-1.5,1.35232071229212,8.3332167220265));
#37547=CARTESIAN_POINT('Ctrl Pts',(-1.5,1.32557926688546,8.33610993612108));
#37548=CARTESIAN_POINT('Ctrl Pts',(-1.5,1.11025704115137,8.35940610762172));
#37549=CARTESIAN_POINT('Ctrl Pts',(-1.5,0.894419768746766,8.37434346908902));
#37550=CARTESIAN_POINT('Ctrl Pts',(-1.5,0.67855625163336,8.38101089356783));
#37551=CARTESIAN_POINT('Ctrl Pts',(-1.5,0.461134916361629,8.38772643472268));
#37552=CARTESIAN_POINT('Ctrl Pts',(-1.5,0.243686264614475,8.38605221878385));
#37553=CARTESIAN_POINT('Ctrl Pts',(-1.5,0.0267066921148425,8.37602648219115));
#37554=CARTESIAN_POINT('Ctrl Pts',(-1.5,-0.18935948302369,8.36604294994628));
#37555=CARTESIAN_POINT('Ctrl Pts',(-1.5,-0.404961196433814,8.34777795012559));
#37556=CARTESIAN_POINT('Ctrl Pts',(-1.5,-0.619601062333341,8.32121848102122));
#37557=CARTESIAN_POINT('Ctrl Pts',(-1.5,-0.832145718967339,8.29491827244855));
#37558=CARTESIAN_POINT('Ctrl Pts',(-1.5,-1.04374783796762,8.26048459624622));
#37559=CARTESIAN_POINT('Ctrl Pts',(-1.5,-1.25390771612789,8.21785690077272));
#37560=CARTESIAN_POINT('Ctrl Pts',(-1.5,-1.38779584224784,8.19069975585181));
#37561=CARTESIAN_POINT('Ctrl Pts',(-1.5,-1.52109824477793,8.16021596832127));
#37562=CARTESIAN_POINT('Ctrl Pts',(-1.5,-1.6536803677507,8.12637995005445));
#37563=CARTESIAN_POINT('Ctrl Pts',(-1.5,-1.71355702926136,8.11109894710169));
#37564=CARTESIAN_POINT('Ctrl Pts',(-1.5,-1.77328671763606,8.09513411894022));
#37565=CARTESIAN_POINT('Ctrl Pts',(-1.5,-1.8328566920054,8.07848259714385));
#37566=CARTESIAN_POINT('Ctrl Pts',(-1.5,-1.85625104511745,8.07194320234166));
#37567=CARTESIAN_POINT('Ctrl Pts',(-1.5,-1.87961849607907,8.06529850226245));
#37568=CARTESIAN_POINT('Ctrl Pts',(-1.5,-1.90294990325727,8.05855087488496));
#37569=CARTESIAN_POINT('Ctrl Pts',(-1.5,-1.95175693881833,8.04443549440875));
#37570=CARTESIAN_POINT('Ctrl Pts',(-1.5,-2.0004168594957,8.02986675849686));
#37571=CARTESIAN_POINT('Ctrl Pts',(-1.5,-2.04892326796492,8.01484480928137));
#37572=CARTESIAN_POINT('Ctrl Pts',(-1.5,-2.25391562363821,7.95136072844197));
#37573=CARTESIAN_POINT('Ctrl Pts',(-1.5,-2.45616780304103,7.87978621926163));
#37574=CARTESIAN_POINT('Ctrl Pts',(-1.5,-2.65527234953228,7.80041100969696));
#37575=CARTESIAN_POINT('Ctrl Pts',(-1.5,-2.85500999528719,7.72078340817231));
#37576=CARTESIAN_POINT('Ctrl Pts',(-1.5,-3.05158055128827,7.63330504161439));
#37577=CARTESIAN_POINT('Ctrl Pts',(-1.5,-3.24454813151519,7.53822212811181));
#37578=CARTESIAN_POINT('Ctrl Pts',(-1.5,-3.34675198073698,7.48786216741915));
#37579=CARTESIAN_POINT('Ctrl Pts',(-1.5,-3.44794465250143,7.43536822680612));
#37580=CARTESIAN_POINT('Ctrl Pts',(-1.5,-3.54805774165375,7.38077220333937));
#37581=CARTESIAN_POINT('Ctrl Pts',(-1.5,-3.62664687830836,7.33791412768357));
#37582=CARTESIAN_POINT('Ctrl Pts',(-1.5,-3.70457069537403,7.29376061887687));
#37583=CARTESIAN_POINT('Ctrl Pts',(-1.5,-3.78179482379092,7.24832583256977));
#37584=CARTESIAN_POINT('Ctrl Pts',(-1.5,-3.80711424857812,7.23342915871656));
#37585=CARTESIAN_POINT('Ctrl Pts',(-1.5,-3.83235671992797,7.218395710483));
#37586=CARTESIAN_POINT('Ctrl Pts',(-1.5,-3.85751122859775,7.2032320690579));
#37587=CARTESIAN_POINT('Ctrl Pts',(-1.5,-4.04011948514428,7.09315215615307));
#37588=CARTESIAN_POINT('Ctrl Pts',(-1.5,-4.21824071284525,6.97612901123971));
#37589=CARTESIAN_POINT('Ctrl Pts',(-1.5,-4.39146092341165,6.85242058055038));
#37590=CARTESIAN_POINT('Ctrl Pts',(-1.5,-4.56386961582583,6.72929171062224));
#37591=CARTESIAN_POINT('Ctrl Pts',(-1.5,-4.73142363312739,6.59953962500907));
#37592=CARTESIAN_POINT('Ctrl Pts',(-1.5,-4.89368134090825,6.46337959276038));
#37593=CARTESIAN_POINT('Ctrl Pts',(-1.5,-5.05352274842095,6.32924722087332));
#37594=CARTESIAN_POINT('Ctrl Pts',(-1.5,-5.20822483934881,6.18889589430103));
#37595=CARTESIAN_POINT('Ctrl Pts',(-1.5,-5.35732594311023,6.04249986337617));
#37596=CARTESIAN_POINT('Ctrl Pts',(-1.5,-5.38967967618284,6.01073310922114));
#37597=CARTESIAN_POINT('Ctrl Pts',(-1.5,-5.42176952083074,5.97868163150745));
#37598=CARTESIAN_POINT('Ctrl Pts',(-1.5,-5.45359047959038,5.94634704090849));
#37599=CARTESIAN_POINT('Ctrl Pts',(-2.3076868253652,-8.92557695889132,-0.000120900814251108));
#37600=CARTESIAN_POINT('Ctrl Pts',(-2.30423366157935,-8.92566437048567,
-0.129190724569353));
#37601=CARTESIAN_POINT('Ctrl Pts',(-2.30078049779349,-8.92292102407511,
-0.258256830648859));
#37602=CARTESIAN_POINT('Ctrl Pts',(-2.29732733400764,-8.91732221770278,
-0.387198950717887));
#37603=CARTESIAN_POINT('Ctrl Pts',(-2.2581810358389,-8.8538521487364,-1.84893288277443));
#37604=CARTESIAN_POINT('Ctrl Pts',(-2.21903473767015,-8.42341836880329,
-3.29473300132172));
#37605=CARTESIAN_POINT('Ctrl Pts',(-2.17988843950141,-7.6770609588897,-4.55316238022893));
#37606=CARTESIAN_POINT('Ctrl Pts',(-2.14074214133266,-6.93070354897609,
-5.81159175913617));
#37607=CARTESIAN_POINT('Ctrl Pts',(-2.10159584316392,-5.868422509082,-6.88265039840332));
#37608=CARTESIAN_POINT('Ctrl Pts',(-2.06244954499517,-4.6161762573865,-7.63933739415508));
#37609=CARTESIAN_POINT('Ctrl Pts',(-2.02330324682643,-3.36393000569105,
-8.39602438990681));
#37610=CARTESIAN_POINT('Ctrl Pts',(-1.98415694865769,-1.92171854219422,
-8.83833974214316));
#37611=CARTESIAN_POINT('Ctrl Pts',(-1.94501065048894,-0.46055735757519,
-8.91383456487796));
#37612=CARTESIAN_POINT('Ctrl Pts',(-1.9058643523202,1.00060382704386,-8.98932938761276));
#37613=CARTESIAN_POINT('Ctrl Pts',(-1.86671805415145,2.48071473278515,-8.698003680846));
#37614=CARTESIAN_POINT('Ctrl Pts',(-1.82757175598271,3.80427888197568,-8.07440367272969));
#37615=CARTESIAN_POINT('Ctrl Pts',(-1.78842545781396,5.1278430311662,-7.4508036646134));
#37616=CARTESIAN_POINT('Ctrl Pts',(-1.74927915964522,6.294860423806,-6.49492935514759));
#37617=CARTESIAN_POINT('Ctrl Pts',(-1.71013286147648,7.16693432419149,-5.32012000128355));
#37618=CARTESIAN_POINT('Ctrl Pts',(-1.67098656330773,8.03900822457701,-4.14531064741947));
#37619=CARTESIAN_POINT('Ctrl Pts',(-1.63184026513899,8.61613863270816,-2.75156624915723));
#37620=CARTESIAN_POINT('Ctrl Pts',(-1.59269396697024,8.82992526135802,-1.30415906014512));
#37621=CARTESIAN_POINT('Ctrl Pts',(-1.56179597798016,8.99866604164268,-0.161727374842938));
#37622=CARTESIAN_POINT('Ctrl Pts',(-1.53089798899008,8.94104834757229,1.01413553490768));
#37623=CARTESIAN_POINT('Ctrl Pts',(-1.5,8.66576000559871,2.13591603404143));
#37624=CARTESIAN_POINT('',(-11.575,-4.68253987355576,-6.57073151046064));
#37625=CARTESIAN_POINT('Ctrl Pts',(-11.575,-4.68274545894496,-6.57070370794207));
#37626=CARTESIAN_POINT('Ctrl Pts',(-11.575,-4.862640076186,-6.45616650491057));
#37627=CARTESIAN_POINT('Ctrl Pts',(-11.575,-5.03774328114105,-6.33464824857975));
#37628=CARTESIAN_POINT('Ctrl Pts',(-11.575,-5.20761491997005,-6.20640283237483));
#37629=CARTESIAN_POINT('Ctrl Pts',(-11.575,-5.26094487773974,-6.16614112254786));
#37630=CARTESIAN_POINT('Ctrl Pts',(-11.575,-5.31375908988843,-6.12521601726515));
#37631=CARTESIAN_POINT('Ctrl Pts',(-11.575,-5.36604355027271,-6.08363438702985));
#37632=CARTESIAN_POINT('Ctrl Pts',(-11.575,-5.53158882597289,-5.95197686602315));
#37633=CARTESIAN_POINT('Ctrl Pts',(-11.575,-5.69182547913848,-5.81374097888015));
#37634=CARTESIAN_POINT('Ctrl Pts',(-11.575,-5.84650148035433,-5.66935359056696));
#37635=CARTESIAN_POINT('Ctrl Pts',(-11.575,-5.95031524401272,-5.57244522671108));
#37636=CARTESIAN_POINT('Ctrl Pts',(-11.575,-6.05162357167362,-5.47276482909323));
#37637=CARTESIAN_POINT('Ctrl Pts',(-11.575,-6.1503422410466,-5.37043108239685));
#37638=CARTESIAN_POINT('Ctrl Pts',(-11.575,-6.18235090099834,-5.33725026543085));
#37639=CARTESIAN_POINT('Ctrl Pts',(-11.575,-6.21408724871341,-5.30379043579792));
#37640=CARTESIAN_POINT('Ctrl Pts',(-11.575,-6.24554824847592,-5.27005547302152));
#37641=CARTESIAN_POINT('Ctrl Pts',(-11.575,-6.27435701813293,-5.23916444033503));
#37642=CARTESIAN_POINT('Ctrl Pts',(-11.575,-6.30293851147707,-5.20803860034052));
#37643=CARTESIAN_POINT('Ctrl Pts',(-11.575,-6.33126902715642,-5.17670480194982));
#37644=CARTESIAN_POINT('Ctrl Pts',(-11.575,-6.47446988673342,-5.01832339745483));
#37645=CARTESIAN_POINT('Ctrl Pts',(-11.575,-6.61135281749366,-4.8545366534807));
#37646=CARTESIAN_POINT('Ctrl Pts',(-11.575,-6.74167674422667,-4.68579125880677));
#37647=CARTESIAN_POINT('Ctrl Pts',(-11.575,-6.87318603173055,-4.51551104104913));
#37648=CARTESIAN_POINT('Ctrl Pts',(-11.575,-6.99801695057332,-4.34018108981283));
#37649=CARTESIAN_POINT('Ctrl Pts',(-11.575,-7.1158880737777,-4.16021989088624));
#37650=CARTESIAN_POINT('Ctrl Pts',(-11.575,-7.23343608965254,-3.98075200008146));
#37651=CARTESIAN_POINT('Ctrl Pts',(-11.575,-7.34406285148296,-3.79667767214885));
#37652=CARTESIAN_POINT('Ctrl Pts',(-11.575,-7.4474489767129,-3.60837960174284));
#37653=CARTESIAN_POINT('Ctrl Pts',(-11.575,-7.46439358665609,-3.57751823278265));
#37654=CARTESIAN_POINT('Ctrl Pts',(-11.575,-7.48114360211281,-3.54654334532797));
#37655=CARTESIAN_POINT('Ctrl Pts',(-11.575,-7.49769750071975,-3.51545655665897));
#37656=CARTESIAN_POINT('Ctrl Pts',(-11.575,-7.51133337928352,-3.48984955704557));
#37657=CARTESIAN_POINT('Ctrl Pts',(-11.575,-7.52483667088816,-3.46416559037544));
#37658=CARTESIAN_POINT('Ctrl Pts',(-11.575,-7.53819861875656,-3.43842107092718));
#37659=CARTESIAN_POINT('Ctrl Pts',(-11.575,-7.63007712735776,-3.2613983737235));
#37660=CARTESIAN_POINT('Ctrl Pts',(-11.575,-7.71536415801572,-3.08134893512341));
#37661=CARTESIAN_POINT('Ctrl Pts',(-11.575,-7.79386964549134,-2.89861723826906));
#37662=CARTESIAN_POINT('Ctrl Pts',(-11.575,-7.87843204090357,-2.70178730318278));
#37663=CARTESIAN_POINT('Ctrl Pts',(-11.575,-7.95512725273153,-2.50184530429948));
#37664=CARTESIAN_POINT('Ctrl Pts',(-11.575,-8.0239739331707,-2.29929720097265));
#37665=CARTESIAN_POINT('Ctrl Pts',(-11.575,-8.09357879607823,-2.09451851194492));
#37666=CARTESIAN_POINT('Ctrl Pts',(-11.575,-8.15516152825037,-1.88707540743478));
#37667=CARTESIAN_POINT('Ctrl Pts',(-11.575,-8.20869509004543,-1.67746392365319));
#37668=CARTESIAN_POINT('Ctrl Pts',(-11.575,-8.26244307268294,-1.46701287176828));
#37669=CARTESIAN_POINT('Ctrl Pts',(-11.575,-8.30807745914933,-1.25437538191467));
#37670=CARTESIAN_POINT('Ctrl Pts',(-11.575,-8.34552150176977,-1.04003606206454));
#37671=CARTESIAN_POINT('Ctrl Pts',(-11.575,-8.37708641586168,-0.859350384340888));
#37672=CARTESIAN_POINT('Ctrl Pts',(-11.575,-8.4028302276656,-0.677454823552394));
#37673=CARTESIAN_POINT('Ctrl Pts',(-11.575,-8.42267840796603,-0.494635356145958));
#37674=CARTESIAN_POINT('Ctrl Pts',(-11.575,-8.42653209511864,-0.459139455659049));
#37675=CARTESIAN_POINT('Ctrl Pts',(-11.575,-8.43016345121736,-0.423608722670985));
#37676=CARTESIAN_POINT('Ctrl Pts',(-11.575,-8.43357181278832,-0.388045248484162));
#37677=CARTESIAN_POINT('Ctrl Pts',(-11.575,-8.43585847597265,-0.364185782451275));
#37678=CARTESIAN_POINT('Ctrl Pts',(-11.575,-8.43804383220084,-0.340321329573578));
#37679=CARTESIAN_POINT('Ctrl Pts',(-11.575,-8.44012789284541,-0.316452872921024));
#37680=CARTESIAN_POINT('Ctrl Pts',(-11.575,-8.45926190081346,-0.0973137413588374));
#37681=CARTESIAN_POINT('Ctrl Pts',(-11.575,-8.46986214320017,0.122169579051059));
#37682=CARTESIAN_POINT('Ctrl Pts',(-11.575,-8.47193372765905,0.341484729619172));
#37683=CARTESIAN_POINT('Ctrl Pts',(-11.575,-8.47401803786911,0.562147133988573));
#37684=CARTESIAN_POINT('Ctrl Pts',(-11.575,-8.46746876336898,0.782639963557231));
#37685=CARTESIAN_POINT('Ctrl Pts',(-11.575,-8.45224135060004,1.00245787088801));
#37686=CARTESIAN_POINT('Ctrl Pts',(-11.575,-8.44874400586925,1.0529443856755));
#37687=CARTESIAN_POINT('Ctrl Pts',(-11.575,-8.44478867456793,1.10339534249771));
#37688=CARTESIAN_POINT('Ctrl Pts',(-11.575,-8.44037443380762,1.15380468310782));
#37689=CARTESIAN_POINT('Ctrl Pts',(-11.575,-8.42125072475744,1.37219185670902));
#37690=CARTESIAN_POINT('Ctrl Pts',(-11.575,-8.3935181125802,1.58979800449828));
#37691=CARTESIAN_POINT('Ctrl Pts',(-11.575,-8.35738688926969,1.80617129702421));
#37692=CARTESIAN_POINT('Ctrl Pts',(-11.575,-8.32111012297363,2.02341617960729));
#37693=CARTESIAN_POINT('Ctrl Pts',(-11.575,-8.27636680539497,2.23941890987782));
#37694=CARTESIAN_POINT('Ctrl Pts',(-11.575,-8.22331761125557,2.45371593671805));
#37695=CARTESIAN_POINT('Ctrl Pts',(-11.575,-8.19399604633327,2.57216305522919));
#37696=CARTESIAN_POINT('Ctrl Pts',(-11.575,-8.1621360953243,2.69008890813614));
#37697=CARTESIAN_POINT('Ctrl Pts',(-11.575,-8.12775833324252,2.80741327792066));
#37698=CARTESIAN_POINT('Ctrl Pts',(-11.575,-8.12030518034422,2.83284938585058));
#37699=CARTESIAN_POINT('Ctrl Pts',(-11.575,-8.11273366594586,2.85825721556884));
#37700=CARTESIAN_POINT('Ctrl Pts',(-11.575,-8.10504397159236,2.883635937813));
#37701=CARTESIAN_POINT('Ctrl Pts',(-11.575,-8.09731580645729,2.90914162729865));
#37702=CARTESIAN_POINT('Ctrl Pts',(-11.575,-8.08947069835413,2.93460986454247));
#37703=CARTESIAN_POINT('Ctrl Pts',(-11.575,-8.08151073061126,2.96003465144566));
#37704=CARTESIAN_POINT('Ctrl Pts',(-11.575,-8.01493466922925,3.17268402744423));
#37705=CARTESIAN_POINT('Ctrl Pts',(-11.575,-7.94029291252216,3.3824100176502));
#37706=CARTESIAN_POINT('Ctrl Pts',(-11.575,-7.857850150231,3.58875907821951));
#37707=CARTESIAN_POINT('Ctrl Pts',(-11.575,-7.77486600628914,3.79646318308773));
#37708=CARTESIAN_POINT('Ctrl Pts',(-11.575,-7.68397791485773,4.00074652093104));
#37709=CARTESIAN_POINT('Ctrl Pts',(-11.575,-7.58540287440055,4.20114269911254));
#37710=CARTESIAN_POINT('Ctrl Pts',(-11.575,-7.48696568741831,4.40125863079959));
#37711=CARTESIAN_POINT('Ctrl Pts',(-11.575,-7.38086282505991,4.59749892632283));
#37712=CARTESIAN_POINT('Ctrl Pts',(-11.575,-7.26726058144177,4.78938542489065));
#37713=CARTESIAN_POINT('Ctrl Pts',(-11.575,-7.20047785200925,4.90218869098355));
#37714=CARTESIAN_POINT('Ctrl Pts',(-11.575,-7.13110252862135,5.01348704406469));
#37715=CARTESIAN_POINT('Ctrl Pts',(-11.575,-7.05916078381547,5.12317972076934));
#37716=CARTESIAN_POINT('Ctrl Pts',(-11.575,-6.9600109611486,5.27435772559069));
#37717=CARTESIAN_POINT('Ctrl Pts',(-11.575,-6.85598705692301,5.42248647666084));
#37718=CARTESIAN_POINT('Ctrl Pts',(-11.575,-6.74727922420573,5.56739584840828));
#37719=CARTESIAN_POINT('Ctrl Pts',(-11.575,-6.69971954739192,5.63079369854779));
#37720=CARTESIAN_POINT('Ctrl Pts',(-11.575,-6.65126310601232,5.69357516367086));
#37721=CARTESIAN_POINT('Ctrl Pts',(-11.575,-6.6019247960547,5.7557251207176));
#37722=CARTESIAN_POINT('Ctrl Pts',(-11.575,-6.57724666313507,5.78681140847788));
#37723=CARTESIAN_POINT('Ctrl Pts',(-11.575,-6.55234789325936,5.81773969543591));
#37724=CARTESIAN_POINT('Ctrl Pts',(-11.575,-6.52723029615612,5.84850803424312));
#37725=CARTESIAN_POINT('Ctrl Pts',(-11.575,-6.51103678232919,5.86834462601018));
#37726=CARTESIAN_POINT('Ctrl Pts',(-11.575,-6.49475776389756,5.88810804101853));
#37727=CARTESIAN_POINT('Ctrl Pts',(-11.575,-6.4783961647675,5.90779520883462));
#37728=CARTESIAN_POINT('Ctrl Pts',(-11.575,-6.33570433488108,6.07948979556954));
#37729=CARTESIAN_POINT('Ctrl Pts',(-11.575,-6.18668135530418,6.24545323529948));
#37730=CARTESIAN_POINT('Ctrl Pts',(-11.575,-6.03177556639099,6.40543183256308));
#37731=CARTESIAN_POINT('Ctrl Pts',(-11.575,-5.87420677232162,6.56816064227763));
#37732=CARTESIAN_POINT('Ctrl Pts',(-11.575,-5.71055082677163,6.72469759373828));
#37733=CARTESIAN_POINT('Ctrl Pts',(-11.575,-5.54123147438693,6.87475116768693));
#37734=CARTESIAN_POINT('Ctrl Pts',(-11.575,-5.37155477858848,7.02512142520189));
#37735=CARTESIAN_POINT('Ctrl Pts',(-11.575,-5.1961902775766,7.16898140035727));
#37736=CARTESIAN_POINT('Ctrl Pts',(-11.575,-5.01552278229665,7.30600572795209));
#37737=CARTESIAN_POINT('Ctrl Pts',(-11.575,-4.83654524178164,7.44174833680182));
#37738=CARTESIAN_POINT('Ctrl Pts',(-11.575,-4.65236293303975,7.57078299743134));
#37739=CARTESIAN_POINT('Ctrl Pts',(-11.575,-4.46331662825554,7.69275536467407));
#37740=CARTESIAN_POINT('Ctrl Pts',(-11.575,-4.2770736438512,7.81291903418392));
#37741=CARTESIAN_POINT('Ctrl Pts',(-11.575,-4.08610934855102,7.92622866201986));
#37742=CARTESIAN_POINT('Ctrl Pts',(-11.575,-3.8907246099259,8.03230272149382));
#37743=CARTESIAN_POINT('Ctrl Pts',(-11.575,-4.68274545894493,-6.57070370794209));
#37744=CARTESIAN_POINT('Ctrl Pts',(-11.5441020110099,-3.83176777330803,
-7.17587091553372));
#37745=CARTESIAN_POINT('Ctrl Pts',(-11.4740577238511,-1.63517269058169,
-8.17393084810367));
#37746=CARTESIAN_POINT('Ctrl Pts',(-11.3648671385235,2.16827971646752,-8.11660023363346));
#37747=CARTESIAN_POINT('Ctrl Pts',(-11.2474282440173,5.74484511045451,-6.13001490910025));
#37748=CARTESIAN_POINT('Ctrl Pts',(-11.129989349511,7.95900894851219,-2.68972043029039));
#37749=CARTESIAN_POINT('Ctrl Pts',(-11.0125504550048,8.28568610932253,1.38846061981056));
#37750=CARTESIAN_POINT('Ctrl Pts',(-10.8951115604986,6.64740134656684,5.1373583652959));
#37751=CARTESIAN_POINT('Ctrl Pts',(-10.7776726659924,3.43267763704583,7.66792930081125));
#37752=CARTESIAN_POINT('Ctrl Pts',(-10.6602337714861,-0.596110146715297,
8.38003913890674));
#37753=CARTESIAN_POINT('Ctrl Pts',(-10.5427948769799,-4.48352951771318,
7.10481331033355));
#37754=CARTESIAN_POINT('Ctrl Pts',(-10.4253559824737,-7.3076743467974,4.14467160188776));
#37755=CARTESIAN_POINT('Ctrl Pts',(-10.3451534671224,-8.05283314175606,
1.45184169729701));
#37756=CARTESIAN_POINT('Ctrl Pts',(-10.3040972499399,-8.0691381443012,0.0645981073621665));
#37757=CARTESIAN_POINT('Ctrl Pts',(-10.3021873309261,-8.06911057618467,
6.34335902037139E-5));
#37758=CARTESIAN_POINT('Origin',(-11.575,-1.70819782223992E-15,-3.76953747432359E-16));
#37759=CARTESIAN_POINT('',(-11.575,-8.925,-1.09299726823901E-15));
#37760=CARTESIAN_POINT('Origin',(-11.575,0.,0.));
#37761=CARTESIAN_POINT('Origin',(-11.575,0.,0.));
#37762=CARTESIAN_POINT('',(-11.575,4.68253987355596,-6.5707315104605));
#37763=CARTESIAN_POINT('Ctrl Pts',(-11.575,3.8909540196873,8.03231038431327));
#37764=CARTESIAN_POINT('Ctrl Pts',(-11.575,4.09069035070338,7.92412861156293));
#37765=CARTESIAN_POINT('Ctrl Pts',(-11.575,4.28601542965074,7.80846352349093));
#37766=CARTESIAN_POINT('Ctrl Pts',(-11.575,4.4764610866747,7.6854730443605));
#37767=CARTESIAN_POINT('Ctrl Pts',(-11.575,4.54451021229802,7.64152667826528));
#37768=CARTESIAN_POINT('Ctrl Pts',(-11.575,4.61193611344074,7.59664463631333));
#37769=CARTESIAN_POINT('Ctrl Pts',(-11.575,4.67871652334774,7.55083278178531));
#37770=CARTESIAN_POINT('Ctrl Pts',(-11.575,4.86632148184985,7.42213439434502));
#37771=CARTESIAN_POINT('Ctrl Pts',(-11.575,5.0488348944294,7.28610053435785));
#37772=CARTESIAN_POINT('Ctrl Pts',(-11.575,5.22591257106765,7.14311556596555));
#37773=CARTESIAN_POINT('Ctrl Pts',(-11.575,5.34391771080921,7.04782991790192));
#37774=CARTESIAN_POINT('Ctrl Pts',(-11.575,5.45950816552951,6.94945650584669));
#37775=CARTESIAN_POINT('Ctrl Pts',(-11.575,5.57257219074754,6.84810087071603));
#37776=CARTESIAN_POINT('Ctrl Pts',(-11.575,5.61416040373507,6.81081934166051));
#37777=CARTESIAN_POINT('Ctrl Pts',(-11.575,5.65540671294731,6.77313426639739));
#37778=CARTESIAN_POINT('Ctrl Pts',(-11.575,5.69630525962318,6.73505070840406));
#37779=CARTESIAN_POINT('Ctrl Pts',(-11.575,5.72899935727988,6.70460689889619));
#37780=CARTESIAN_POINT('Ctrl Pts',(-11.575,5.76147534498076,6.67390437527803));
#37781=CARTESIAN_POINT('Ctrl Pts',(-11.575,5.79370643387823,6.64296877678564));
#37782=CARTESIAN_POINT('Ctrl Pts',(-11.575,5.95657310025678,6.48664834296758));
#37783=CARTESIAN_POINT('Ctrl Pts',(-11.575,6.11328907427985,6.32428998283107));
#37784=CARTESIAN_POINT('Ctrl Pts',(-11.575,6.2635341324018,6.15628508681688));
#37785=CARTESIAN_POINT('Ctrl Pts',(-11.575,6.41336099455174,5.98874781996579));
#37786=CARTESIAN_POINT('Ctrl Pts',(-11.575,6.55675331297687,5.81559485699136));
#37787=CARTESIAN_POINT('Ctrl Pts',(-11.575,6.69335279993625,5.63718293709442));
#37788=CARTESIAN_POINT('Ctrl Pts',(-11.575,6.82873374273438,5.46036255174955));
#37789=CARTESIAN_POINT('Ctrl Pts',(-11.575,6.95744284599461,5.27837607658992));
#37790=CARTESIAN_POINT('Ctrl Pts',(-11.575,7.07908582397012,5.09154805860869));
#37791=CARTESIAN_POINT('Ctrl Pts',(-11.575,7.10207551861353,5.05623883520997));
#37792=CARTESIAN_POINT('Ctrl Pts',(-11.575,7.12481268216614,5.02075662710973));
#37793=CARTESIAN_POINT('Ctrl Pts',(-11.575,7.14729445264254,4.9851035570856));
#37794=CARTESIAN_POINT('Ctrl Pts',(-11.575,7.1681591197164,4.95201499597806));
#37795=CARTESIAN_POINT('Ctrl Pts',(-11.575,7.18880670503735,4.91877440480665));
#37796=CARTESIAN_POINT('Ctrl Pts',(-11.575,7.20921801861532,4.88541141690287));
#37797=CARTESIAN_POINT('Ctrl Pts',(-11.575,7.31755469203634,4.70833143079254));
#37798=CARTESIAN_POINT('Ctrl Pts',(-11.575,7.41931816251136,4.52768181901124));
#37799=CARTESIAN_POINT('Ctrl Pts',(-11.575,7.51425932679982,4.3437592816672));
#37800=CARTESIAN_POINT('Ctrl Pts',(-11.575,7.61605469031111,4.14655860810088));
#37801=CARTESIAN_POINT('Ctrl Pts',(-11.575,7.71000799576338,3.94559518439185));
#37802=CARTESIAN_POINT('Ctrl Pts',(-11.575,7.79604523983125,3.74136883761279));
#37803=CARTESIAN_POINT('Ctrl Pts',(-11.575,7.88244746162894,3.53627614429712));
#37804=CARTESIAN_POINT('Ctrl Pts',(-11.575,7.96086647438103,3.3278921106263));
#37805=CARTESIAN_POINT('Ctrl Pts',(-11.575,8.03117746555899,3.11670639005853));
#37806=CARTESIAN_POINT('Ctrl Pts',(-11.575,8.10121298627027,2.90634807112496));
#37807=CARTESIAN_POINT('Ctrl Pts',(-11.575,8.1632039896943,2.69320929856103));
#37808=CARTESIAN_POINT('Ctrl Pts',(-11.575,8.21697596967883,2.4777677535818));
#37809=CARTESIAN_POINT('Ctrl Pts',(-11.575,8.26188761707955,2.29782580786291));
#37810=CARTESIAN_POINT('Ctrl Pts',(-11.575,8.30106482476432,2.11627714880915));
#37811=CARTESIAN_POINT('Ctrl Pts',(-11.575,8.33437760016051,1.93340186433423));
#37812=CARTESIAN_POINT('Ctrl Pts',(-11.575,8.3410674207946,1.89667712924399));
#37813=CARTESIAN_POINT('Ctrl Pts',(-11.575,8.34752065536839,1.85989890749364));
#37814=CARTESIAN_POINT('Ctrl Pts',(-11.575,8.35373612235081,1.82306949144067));
#37815=CARTESIAN_POINT('Ctrl Pts',(-11.575,8.35791106064617,1.79833111861849));
#37816=CARTESIAN_POINT('Ctrl Pts',(-11.575,8.36197777909343,1.7735750980682));
#37817=CARTESIAN_POINT('Ctrl Pts',(-11.575,8.3659349176602,1.74880967041789));
#37818=CARTESIAN_POINT('Ctrl Pts',(-11.575,8.40065470151849,1.53151874651718));
#37819=CARTESIAN_POINT('Ctrl Pts',(-11.575,8.42697311679527,1.31332666260153));
#37820=CARTESIAN_POINT('Ctrl Pts',(-11.575,8.44480476752567,1.09470887941076));
#37821=CARTESIAN_POINT('Ctrl Pts',(-11.575,8.46257370213098,0.876860002051726));
#37822=CARTESIAN_POINT('Ctrl Pts',(-11.575,8.47191553606587,0.65858774848646));
#37823=CARTESIAN_POINT('Ctrl Pts',(-11.575,8.47269453239138,0.440357329235993));
#37824=CARTESIAN_POINT('Ctrl Pts',(-11.575,8.47289362379682,0.384583252443501));
#37825=CARTESIAN_POINT('Ctrl Pts',(-11.575,8.47253314142673,0.328811909903161));
#37826=CARTESIAN_POINT('Ctrl Pts',(-11.575,8.47161027062858,0.273051092863091));
#37827=CARTESIAN_POINT('Ctrl Pts',(-11.575,8.46798133197079,0.0537868307881026));
#37828=CARTESIAN_POINT('Ctrl Pts',(-11.575,8.4556604711072,-0.165315593783987));
#37829=CARTESIAN_POINT('Ctrl Pts',(-11.575,8.43476764154084,-0.383762556599518));
#37830=CARTESIAN_POINT('Ctrl Pts',(-11.575,8.41395932183961,-0.601325918497957));
#37831=CARTESIAN_POINT('Ctrl Pts',(-11.575,8.3846480034043,-0.818239764904438));
#37832=CARTESIAN_POINT('Ctrl Pts',(-11.575,8.34690369724573,-1.03399926810862));
#37833=CARTESIAN_POINT('Ctrl Pts',(-11.575,8.32669936168747,-1.14949423533114));
#37834=CARTESIAN_POINT('Ctrl Pts',(-11.575,8.30407782627792,-1.26465808454184));
#37835=CARTESIAN_POINT('Ctrl Pts',(-11.575,8.27904443208135,-1.37941035657947));
#37836=CARTESIAN_POINT('Ctrl Pts',(-11.575,8.27346937299148,-1.40496624773363));
#37837=CARTESIAN_POINT('Ctrl Pts',(-11.575,8.26777467745199,-1.4305017159728));
#37838=CARTESIAN_POINT('Ctrl Pts',(-11.575,8.26196037991734,-1.45601585527642));
#37839=CARTESIAN_POINT('Ctrl Pts',(-11.575,8.25632839154964,-1.48072999054615));
#37840=CARTESIAN_POINT('Ctrl Pts',(-11.575,8.25058629462981,-1.50541481702675));
#37841=CARTESIAN_POINT('Ctrl Pts',(-11.575,8.24473496759404,-1.53006711391079));
#37842=CARTESIAN_POINT('Ctrl Pts',(-11.575,8.19462468872943,-1.74118733740221));
#37843=CARTESIAN_POINT('Ctrl Pts',(-11.575,8.13649408842284,-1.94998221456258));
#37844=CARTESIAN_POINT('Ctrl Pts',(-11.575,8.07050941331969,-2.15598886710096));
#37845=CARTESIAN_POINT('Ctrl Pts',(-11.575,8.00454781312325,-2.36192347890745));
#37846=CARTESIAN_POINT('Ctrl Pts',(-11.575,7.93073739624093,-2.56507246994707));
#37847=CARTESIAN_POINT('Ctrl Pts',(-11.575,7.8491944550522,-2.76495843616166));
#37848=CARTESIAN_POINT('Ctrl Pts',(-11.575,7.7685709179915,-2.96259066980547));
#37849=CARTESIAN_POINT('Ctrl Pts',(-11.575,7.68038795006705,-3.15703362359616));
#37850=CARTESIAN_POINT('Ctrl Pts',(-11.575,7.58471333576317,-3.34780208001595));
#37851=CARTESIAN_POINT('Ctrl Pts',(-11.575,7.53014632821733,-3.45660485781346));
#37852=CARTESIAN_POINT('Ctrl Pts',(-11.575,7.47314159064295,-3.56421188609963));
#37853=CARTESIAN_POINT('Ctrl Pts',(-11.575,7.41370561910289,-3.67052853101672));
#37854=CARTESIAN_POINT('Ctrl Pts',(-11.575,7.33195298620427,-3.81676431075931));
#37855=CARTESIAN_POINT('Ctrl Pts',(-11.575,7.24560098255595,-3.96055936581355));
#37856=CARTESIAN_POINT('Ctrl Pts',(-11.575,7.1547904636629,-4.10172616067142));
#37857=CARTESIAN_POINT('Ctrl Pts',(-11.575,7.11506086164719,-4.16348663342174));
#37858=CARTESIAN_POINT('Ctrl Pts',(-11.575,7.07447771520422,-4.22474385495871));
#37859=CARTESIAN_POINT('Ctrl Pts',(-11.575,7.03305213420888,-4.28548120740034));
#37860=CARTESIAN_POINT('Ctrl Pts',(-11.575,7.00995571903755,-4.31934470610558));
#37861=CARTESIAN_POINT('Ctrl Pts',(-11.575,6.98659742541435,-4.35304659275271));
#37862=CARTESIAN_POINT('Ctrl Pts',(-11.575,6.96297912814017,-4.38658390647314));
#37863=CARTESIAN_POINT('Ctrl Pts',(-11.575,6.94725346269133,-4.40891390636678));
#37864=CARTESIAN_POINT('Ctrl Pts',(-11.575,6.93141725469661,-4.43116419555797));
#37865=CARTESIAN_POINT('Ctrl Pts',(-11.575,6.91547562163386,-4.45332807617772));
#37866=CARTESIAN_POINT('Ctrl Pts',(-11.575,6.79134840278254,-4.62590392517971));
#37867=CARTESIAN_POINT('Ctrl Pts',(-11.575,6.66075184134787,-4.79335902618009));
#37868=CARTESIAN_POINT('Ctrl Pts',(-11.575,6.52405945291491,-4.95538312636472));
#37869=CARTESIAN_POINT('Ctrl Pts',(-11.575,6.38652067756353,-5.11841046513812));
#37870=CARTESIAN_POINT('Ctrl Pts',(-11.575,6.2428098747442,-5.27593983973574));
#37871=CARTESIAN_POINT('Ctrl Pts',(-11.575,6.09326686075735,-5.42762206125614));
#37872=CARTESIAN_POINT('Ctrl Pts',(-11.575,5.94445087436889,-5.57856685507403));
#37873=CARTESIAN_POINT('Ctrl Pts',(-11.575,5.78985872238046,-5.72372164315627));
#37874=CARTESIAN_POINT('Ctrl Pts',(-11.575,5.62979274260417,-5.86270269648403));
#37875=CARTESIAN_POINT('Ctrl Pts',(-11.575,5.47264807795008,-5.99914724921779));
#37876=CARTESIAN_POINT('Ctrl Pts',(-11.575,5.31022703737972,-6.12964166221526));
#37877=CARTESIAN_POINT('Ctrl Pts',(-11.575,5.14279211761008,-6.25377930689961));
#37878=CARTESIAN_POINT('Ctrl Pts',(-11.575,4.99331293730095,-6.36460441673007));
#37879=CARTESIAN_POINT('Ctrl Pts',(-11.575,4.83983707019304,-6.47036267996695));
#37880=CARTESIAN_POINT('Ctrl Pts',(-11.575,4.68253987355598,-6.57073151046049));
#37881=CARTESIAN_POINT('Origin',(-11.575,0.,0.));
#37882=CARTESIAN_POINT('Origin',(-14.3478126690739,0.,0.));
#37883=CARTESIAN_POINT('Ctrl Pts',(-11.575,4.68253987355595,-6.57073151046051));
#37884=CARTESIAN_POINT('Ctrl Pts',(-11.5358537018313,5.75997971466614,-5.80290908318214));
#37885=CARTESIAN_POINT('Ctrl Pts',(-11.4575611054938,7.52902184303394,-3.72801696096832));
#37886=CARTESIAN_POINT('Ctrl Pts',(-11.3401222109875,8.39684879745447,0.270811863526706));
#37887=CARTESIAN_POINT('Ctrl Pts',(-11.2226833164813,7.27339149706363,4.20443640376082));
#37888=CARTESIAN_POINT('Ctrl Pts',(-11.1052444219751,4.42502579862193,7.14145324703773));
#37889=CARTESIAN_POINT('Ctrl Pts',(-10.9878055274688,0.527266627263149,
8.38462365194841));
#37890=CARTESIAN_POINT('Ctrl Pts',(-10.8703666329626,-3.49553795222623,
7.63949276732611));
#37891=CARTESIAN_POINT('Ctrl Pts',(-10.7529277384564,-6.68936958853091,
5.08258437974203));
#37892=CARTESIAN_POINT('Ctrl Pts',(-10.6620764171601,-7.93289342748698,
2.17211355225587));
#37893=CARTESIAN_POINT('Ctrl Pts',(-10.6103713940326,-8.0685071350501,0.424666440026747));
#37894=CARTESIAN_POINT('Ctrl Pts',(-10.5978126690739,-8.06816497465237,
0.000173167597293036));
#37895=CARTESIAN_POINT('Ctrl Pts',(-12.0695005055609,5.17960815163744,-7.26823805302846));
#37896=CARTESIAN_POINT('Ctrl Pts',(-12.0303542073922,6.37142206771955,-6.41890854153817));
#37897=CARTESIAN_POINT('Ctrl Pts',(-11.9520616110547,8.32825431605352,-4.12375923364224));
#37898=CARTESIAN_POINT('Ctrl Pts',(-11.8346227165484,9.28820419127237,0.299559506968546));
#37899=CARTESIAN_POINT('Ctrl Pts',(-11.7171838220422,8.04548789877833,4.65075229640766));
#37900=CARTESIAN_POINT('Ctrl Pts',(-11.599744927536,4.89475804086272,7.89954393379335));
#37901=CARTESIAN_POINT('Ctrl Pts',(-11.4823060330297,0.583237856890839,
9.2746813030476));
#37902=CARTESIAN_POINT('Ctrl Pts',(-11.3648671385235,-3.86660175046402,
8.45045212225142));
#37903=CARTESIAN_POINT('Ctrl Pts',(-11.2474282440173,-7.39946998545434,
5.62211880637018));
#37904=CARTESIAN_POINT('Ctrl Pts',(-11.1299893495111,-9.17754567157279,
1.4605279695957));
#37905=CARTESIAN_POINT('Ctrl Pts',(-11.0125504550048,-8.77915445415917,
-3.04744664874868));
#37906=CARTESIAN_POINT('Ctrl Pts',(-10.8951115604986,-6.29877606274185,
-6.83270648092648));
#37907=CARTESIAN_POINT('Ctrl Pts',(-10.7776726659923,-2.32463494290788,
-8.99758602485665));
#37908=CARTESIAN_POINT('Ctrl Pts',(-10.6602337714861,2.20079618741207,-9.0286744979603));
#37909=CARTESIAN_POINT('Ctrl Pts',(-10.5427948769799,6.20430579028754,-6.91860273246797));
#37910=CARTESIAN_POINT('Ctrl Pts',(-10.4253559824737,8.7364565199315,-3.16777510115142));
#37911=CARTESIAN_POINT('Ctrl Pts',(-10.3079170879674,9.1967456981277,1.33429404234123));
#37912=CARTESIAN_POINT('Ctrl Pts',(-10.1904781934612,7.47601515924667,5.5199338438618));
#37913=CARTESIAN_POINT('Ctrl Pts',(-10.073039298955,3.98233830328959,8.39651437135721));
#37914=CARTESIAN_POINT('Ctrl Pts',(-9.95560040444873,-0.455755049286878,
9.28185108312358));
#37915=CARTESIAN_POINT('Ctrl Pts',(-9.83816150994249,-4.78576552292591,
7.96598521377529));
#37916=CARTESIAN_POINT('Ctrl Pts',(-9.72072261543627,-7.98082573416653,
4.76097602585856));
#37917=CARTESIAN_POINT('Ctrl Pts',(-9.60328372093003,-9.28322316851808,
0.426895430196007));
#37918=CARTESIAN_POINT('Ctrl Pts',(-9.4858448264238,-8.38409265026308,-4.00842394652925));
#37919=CARTESIAN_POINT('Ctrl Pts',(-9.36840593191757,-5.49666410311126,
-7.49314058627073));
#37920=CARTESIAN_POINT('Ctrl Pts',(-9.25096703741133,-1.30569480834948,
-9.2008495896654));
#37921=CARTESIAN_POINT('Ctrl Pts',(-9.13352814290511,3.19492163871721,-8.72656563768809));
#37922=CARTESIAN_POINT('Ctrl Pts',(-9.01608924839887,6.93785843437135,-6.18276576056752));
#37923=CARTESIAN_POINT('Ctrl Pts',(-8.89865035389264,9.03547344924704,-2.17271527211811));
#37924=CARTESIAN_POINT('Ctrl Pts',(-8.78121145938641,8.9903146663651,2.35259735302393));
#37925=CARTESIAN_POINT('Ctrl Pts',(-8.66377256488017,6.81309154741103,6.31998858165539));
#37926=CARTESIAN_POINT('Ctrl Pts',(-8.54633367037394,3.0201352705307,8.78858663571183));
#37927=CARTESIAN_POINT('Ctrl Pts',(-8.42889477586771,-1.48904985254373,
9.17296040775923));
#37928=CARTESIAN_POINT('Ctrl Pts',(-8.31145588136147,-5.64510494590745,
7.38195517836491));
#37929=CARTESIAN_POINT('Ctrl Pts',(-8.19401698685524,-8.46241636063372,
3.84031007146154));
#37930=CARTESIAN_POINT('Ctrl Pts',(-8.07657809234901,-9.27285518089936,
-0.612069358618491));
#37931=CARTESIAN_POINT('Ctrl Pts',(-7.95913919784278,-7.88422482967884,
-4.9192957769144));
#37932=CARTESIAN_POINT('Ctrl Pts',(-7.84170030333655,-4.6258407266985,-8.05990506624669));
#37933=CARTESIAN_POINT('Ctrl Pts',(-7.72426140883031,-0.270432725917864,
-9.28909781660439));
#37934=CARTESIAN_POINT('Ctrl Pts',(-7.60682251432408,4.14910873310461,-8.31536943416027));
#37935=CARTESIAN_POINT('Ctrl Pts',(-7.48938361981784,7.58468388119963,-5.36964081926924));
#37936=CARTESIAN_POINT('Ctrl Pts',(-7.37194472531162,9.22154178706155,-1.1504951869388));
#37937=CARTESIAN_POINT('Ctrl Pts',(-7.25450583080538,8.67149955678534,3.34149181390041));
#37938=CARTESIAN_POINT('Ctrl Pts',(-7.13706693629915,6.06500039130734,7.04103986348135));
#37939=CARTESIAN_POINT('Ctrl Pts',(-7.01962804179292,2.02017881861132,9.0707965276775));
#37940=CARTESIAN_POINT('Ctrl Pts',(-6.90218914728668,-2.50373068053572,
8.94940248201162));
#37941=CARTESIAN_POINT('Ctrl Pts',(-6.78475025278046,-6.43387732607846,
6.70564647581913));
#37942=CARTESIAN_POINT('Ctrl Pts',(-6.66731135827422,-8.83822193924971,
2.87163804443684));
#37943=CARTESIAN_POINT('Ctrl Pts',(-6.54987246376798,-9.14657119627741,
-1.64338293076208));
#37944=CARTESIAN_POINT('Ctrl Pts',(-6.43243356926176,-7.28579968627662,
-5.76867359426266));
#37945=CARTESIAN_POINT('Ctrl Pts',(-6.31499467475552,-3.69719169364456,
-8.52591612005052));
#37946=CARTESIAN_POINT('Ctrl Pts',(-6.1975557802493,0.768209920364817,-9.26122700423357));
#37947=CARTESIAN_POINT('Ctrl Pts',(-6.08011688574306,5.05142959362918,-7.8002263535297));
#37948=CARTESIAN_POINT('Ctrl Pts',(-5.96267799123683,8.1366964384956,-4.48939229444975));
#37949=CARTESIAN_POINT('Ctrl Pts',(-5.8452390967306,9.29233557468242,-0.113893253459215));
#37950=CARTESIAN_POINT('Ctrl Pts',(-5.72780020222436,8.24428573970098,4.28861571463967));
#37951=CARTESIAN_POINT('Ctrl Pts',(-5.61036130771813,5.24109325907115,7.67407411714348));
#37952=CARTESIAN_POINT('Ctrl Pts',(-5.4929224132119,0.994968975230345,9.23961627147041));
#37953=CARTESIAN_POINT('Ctrl Pts',(-5.37548351870567,-3.487113442036,8.61397190313867));
#37954=CARTESIAN_POINT('Ctrl Pts',(-5.25804462419943,-7.14222255730959,
5.94551335441738));
#37955=CARTESIAN_POINT('Ctrl Pts',(-5.14060572969321,-9.10354468515787,
1.86706889830364));
#37956=CARTESIAN_POINT('Ctrl Pts',(-5.02316683518696,-8.90594983675637,
-2.65415327569744));
#37957=CARTESIAN_POINT('Ctrl Pts',(-4.90572794068074,-6.5962978768398,-6.5459396900412));
#37958=CARTESIAN_POINT('Ctrl Pts',(-4.7882890461745,-2.72232564837539,-8.88534834263194));
#37959=CARTESIAN_POINT('Ctrl Pts',(-4.67085015166827,1.79724950297649,-9.11758555374142));
#37960=CARTESIAN_POINT('Ctrl Pts',(-4.55341125716204,5.89060469307803,-7.18757597909831));
#37961=CARTESIAN_POINT('Ctrl Pts',(-4.43597236265581,8.58699563339623,-3.55302379649448));
#37962=CARTESIAN_POINT('Ctrl Pts',(-4.31853346814957,9.24696984916455,0.924132410879959));
#37963=CARTESIAN_POINT('Ctrl Pts',(-4.20109457364334,7.7140136324976,5.18212946438919));
#37964=CARTESIAN_POINT('Ctrl Pts',(-4.08365567913711,4.35166946109418,8.21117805218502));
#37965=CARTESIAN_POINT('Ctrl Pts',(-3.96621678463088,-0.0426785491791672,
9.29293552362616));
#37966=CARTESIAN_POINT('Ctrl Pts',(-3.84877789012465,-4.42690529092247,
8.17086174544261));
#37967=CARTESIAN_POINT('Ctrl Pts',(-3.73133899561841,-7.76128591638191,
5.11105791306308));
#37968=CARTESIAN_POINT('Ctrl Pts',(-3.61390010111218,-9.25506791693505,
0.839160322675105));
#37969=CARTESIAN_POINT('Ctrl Pts',(-3.49646120660595,-8.55399899768065,
-3.63174518626155));
#37970=CARTESIAN_POINT('Ctrl Pts',(-3.37902231209972,-5.82433858706542,
-7.24137779190658));
#37971=CARTESIAN_POINT('Ctrl Pts',(-3.26158341759348,-1.71342893807153,
-9.13370862802382));
#37972=CARTESIAN_POINT('Ctrl Pts',(-3.14414452308726,2.80382236659545,-8.85996906048253));
#37973=CARTESIAN_POINT('Ctrl Pts',(-3.02670562858102,6.65614400340243,-6.4850768010162));
#37974=CARTESIAN_POINT('Ctrl Pts',(-2.90926673407479,8.92995219053902,-2.5722404481956));
#37975=CARTESIAN_POINT('Ctrl Pts',(-2.79182783956855,9.08601225502845,1.95060585305106));
#37976=CARTESIAN_POINT('Ctrl Pts',(-2.67438894506232,7.08731086261654,6.01086370496802));
#37977=CARTESIAN_POINT('Ctrl Pts',(-2.55695005055609,3.40784942603698,8.64563741411886));
#37978=CARTESIAN_POINT('Ctrl Pts',(-2.43951115604986,-1.07979674662018,
9.23008805428009));
#37979=CARTESIAN_POINT('Ctrl Pts',(-2.32207226154363,-5.31135005799377,
7.62561056572066));
#37980=CARTESIAN_POINT('Ctrl Pts',(-2.20463336703739,-8.28334497403523,
4.21271245259873));
#37981=CARTESIAN_POINT('Ctrl Pts',(-2.08719447253116,-9.29086556292747,
-0.199240463811235));
#37982=CARTESIAN_POINT('Ctrl Pts',(-1.96975557802493,-8.09518120960245,
-4.56393381023661));
#37983=CARTESIAN_POINT('Ctrl Pts',(-1.8523166835187,-4.97944750926598,-7.84630326678714));
#37984=CARTESIAN_POINT('Ctrl Pts',(-1.73487778901247,-0.683361058726897,
-9.26787411763888));
#37985=CARTESIAN_POINT('Ctrl Pts',(-1.61743889450623,3.77586765201595,-8.49164493160031));
#37986=CARTESIAN_POINT('Ctrl Pts',(-1.53914629816874,6.14996708109111,-6.63138831099122));
#37987=CARTESIAN_POINT('Ctrl Pts',(-1.5,7.04785050324084,-5.47571258230085));
#37988=CARTESIAN_POINT('Ctrl Pts',(-11.9046670037073,5.01391872561028,-7.03573587217248));
#37989=CARTESIAN_POINT('Ctrl Pts',(-11.8655207055385,6.16760795003508,-6.21357538875283));
#37990=CARTESIAN_POINT('Ctrl Pts',(-11.787228109201,8.06184349171365,-3.99184514275093));
#37991=CARTESIAN_POINT('Ctrl Pts',(-11.6697892146948,8.99108572666641,0.289976959154598));
#37992=CARTESIAN_POINT('Ctrl Pts',(-11.5523503201886,7.7881224315401,4.50198033219205));
#37993=CARTESIAN_POINT('Ctrl Pts',(-11.4349114256823,4.73818062678245,7.64684703820814));
#37994=CARTESIAN_POINT('Ctrl Pts',(-11.3174725311761,0.564580780348278,
8.97799541934787));
#37995=CARTESIAN_POINT('Ctrl Pts',(-11.2000336366699,-3.7429138177181,8.18013233727632));
#37996=CARTESIAN_POINT('Ctrl Pts',(-11.0825947421636,-7.16276985314653,
5.44227399749412));
#37997=CARTESIAN_POINT('Ctrl Pts',(-10.9651558476574,-8.88396703972585,
1.41380743902767));
#37998=CARTESIAN_POINT('Ctrl Pts',(-10.8477169531512,-8.4983198775023,-2.94996250104922));
#37999=CARTESIAN_POINT('Ctrl Pts',(-10.730278058645,-6.09728580325582,-6.6141364304722));
#38000=CARTESIAN_POINT('Ctrl Pts',(-10.6128391641387,-2.25027267106471,
-8.70976408535003));
#38001=CARTESIAN_POINT('Ctrl Pts',(-10.4954002696325,2.1303953681957,-8.73985807564459));
#38002=CARTESIAN_POINT('Ctrl Pts',(-10.3779613751262,6.00583752102961,-6.69728496438734));
#38003=CARTESIAN_POINT('Ctrl Pts',(-10.26052248062,8.4569877987617,-3.06644179119301));
#38004=CARTESIAN_POINT('Ctrl Pts',(-10.1430835861138,8.90255288055735,1.29161158305961));
#38005=CARTESIAN_POINT('Ctrl Pts',(-10.0256446916076,7.2368664390265,5.34335780885649));
#38006=CARTESIAN_POINT('Ctrl Pts',(-9.90820579710132,3.85494809762134,8.12791999006617));
#38007=CARTESIAN_POINT('Ctrl Pts',(-9.79076690259508,-0.44117599420886,
8.9849358467951));
#38008=CARTESIAN_POINT('Ctrl Pts',(-9.67332800808886,-4.63267464821495,
7.71116294167077));
#38009=CARTESIAN_POINT('Ctrl Pts',(-9.55588911358262,-7.72552873168984,
4.60867813730028));
#38010=CARTESIAN_POINT('Ctrl Pts',(-9.43845021907639,-8.98626404083047,
0.413239559571804));
#38011=CARTESIAN_POINT('Ctrl Pts',(-9.32101132457016,-8.11589562486812,
-3.88019929255345));
#38012=CARTESIAN_POINT('Ctrl Pts',(-9.20357243006392,-5.32083243908456,
-7.25344404426735));
#38013=CARTESIAN_POINT('Ctrl Pts',(-9.0861335355577,-1.263927204116,-8.90652549354782));
#38014=CARTESIAN_POINT('Ctrl Pts',(-8.96869464105145,3.09271994371959,-8.44741331392787));
#38015=CARTESIAN_POINT('Ctrl Pts',(-8.85125574654525,6.71592469957997,-5.98498653091574));
#38016=CARTESIAN_POINT('Ctrl Pts',(-8.73381685203898,8.7464395366689,-2.10321272755903));
#38017=CARTESIAN_POINT('Ctrl Pts',(-8.61637795753279,8.7027253288584,2.27734059736138));
#38018=CARTESIAN_POINT('Ctrl Pts',(-8.49893906302652,6.59514895505407,6.11781975923941));
#38019=CARTESIAN_POINT('Ctrl Pts',(-8.38150016852031,2.92352478092436,8.507450334928));
#38020=CARTESIAN_POINT('Ctrl Pts',(-8.26406127401406,-1.4414169412943,8.8795284529788));
#38021=CARTESIAN_POINT('Ctrl Pts',(-8.14662237950784,-5.464524838114,7.14581532363963));
#38022=CARTESIAN_POINT('Ctrl Pts',(-8.0291834850016,-8.19171385408349,3.71746317785904));
#38023=CARTESIAN_POINT('Ctrl Pts',(-7.91174459049538,-8.97622771264762,
-0.592489997062687));
#38024=CARTESIAN_POINT('Ctrl Pts',(-7.79430569598914,-7.63201797378267,
-4.76193343021311));
#38025=CARTESIAN_POINT('Ctrl Pts',(-7.67686680148291,-4.47786565359234,
-7.80207841118636));
#38026=CARTESIAN_POINT('Ctrl Pts',(-7.55942790697667,-0.261781908747044,
-8.99195076600041));
#38027=CARTESIAN_POINT('Ctrl Pts',(-7.44198901247044,4.01638374225852,-8.04937078167256));
#38028=CARTESIAN_POINT('Ctrl Pts',(-7.32455011796421,7.34205897945369,-5.19787247709541));
#38029=CARTESIAN_POINT('Ctrl Pts',(-7.20711122345798,8.92655577247263,-1.11369223165913));
#38030=CARTESIAN_POINT('Ctrl Pts',(-7.08967232895174,8.39410873062712,3.2346015155398));
#38031=CARTESIAN_POINT('Ctrl Pts',(-6.97223343444552,5.87098833397195,6.81580547905291));
#38032=CARTESIAN_POINT('Ctrl Pts',(-6.85479453993928,1.95555573147255,8.78063267236637));
#38033=CARTESIAN_POINT('Ctrl Pts',(-6.73735564543305,-2.42363935176341,
8.66312187600441));
#38034=CARTESIAN_POINT('Ctrl Pts',(-6.61991675092681,-6.22806533990531,
6.49114092188676));
#38035=CARTESIAN_POINT('Ctrl Pts',(-6.50247785642058,-8.55549786489052,
2.77977780223104));
#38036=CARTESIAN_POINT('Ctrl Pts',(-6.38503896191435,-8.85398340058697,
-1.59081309023183));
#38037=CARTESIAN_POINT('Ctrl Pts',(-6.26760006740812,-7.05273572992569,
-5.58414067424452));
#38038=CARTESIAN_POINT('Ctrl Pts',(-6.15016117290189,-3.57892298456495,
-8.25318233268084));
#38039=CARTESIAN_POINT('Ctrl Pts',(-6.03272227839566,0.743635810307214,
-8.96497150734744));
#38040=CARTESIAN_POINT('Ctrl Pts',(-5.91528338388941,4.88984044528396,-7.5507065077109));
#38041=CARTESIAN_POINT('Ctrl Pts',(-5.79784448938319,7.87641331993083,-4.34578204234158));
#38042=CARTESIAN_POINT('Ctrl Pts',(-5.68040559487695,8.99508495209735,-0.110249945463397));
#38043=CARTESIAN_POINT('Ctrl Pts',(-5.56296670037073,7.98056096898001,4.1514280634879));
#38044=CARTESIAN_POINT('Ctrl Pts',(-5.44552780586449,5.07343699851486,7.42858972941861));
#38045=CARTESIAN_POINT('Ctrl Pts',(-5.32808891135826,0.963141116134738,
8.94405207589564));
#38046=CARTESIAN_POINT('Ctrl Pts',(-5.21065001685203,-3.37556488318993,
8.33842131732958));
#38047=CARTESIAN_POINT('Ctrl Pts',(-5.09321112234579,-6.91375146037828,
5.75532354347215));
#38048=CARTESIAN_POINT('Ctrl Pts',(-4.97577222783957,-8.8123332557335,1.80734361309739));
#38049=CARTESIAN_POINT('Ctrl Pts',(-4.85833333333333,-8.62105922853295,
-2.56925010928718));
#38050=CARTESIAN_POINT('Ctrl Pts',(-4.7408944388271,-6.38529025288039,-6.33654296382196));
#38051=CARTESIAN_POINT('Ctrl Pts',(-4.62345554432087,-2.63524172987553,
-8.60111675139145));
#38052=CARTESIAN_POINT('Ctrl Pts',(-4.50601664981463,1.73975765613059,-8.82592497384302));
#38053=CARTESIAN_POINT('Ctrl Pts',(-4.3885777553084,5.70217134407256,-6.95765408083135));
#38054=CARTESIAN_POINT('Ctrl Pts',(-4.27113886080217,8.31230798596378,-3.43936684479708));
#38055=CARTESIAN_POINT('Ctrl Pts',(-4.15369996629594,8.9511704214966,0.894570528156575));
#38056=CARTESIAN_POINT('Ctrl Pts',(-4.0362610717897,7.46725162778297,5.01635938460398));
#38057=CARTESIAN_POINT('Ctrl Pts',(-3.91882217728347,4.21246479654041,7.94851235651008));
#38058=CARTESIAN_POINT('Ctrl Pts',(-3.80138328277724,-0.0413133137964638,
8.99566570939701));
#38059=CARTESIAN_POINT('Ctrl Pts',(-3.68394438827101,-4.28529392279269,
7.9094857198601));
#38060=CARTESIAN_POINT('Ctrl Pts',(-3.56650549376477,-7.51301172824443,
4.94756132660039));
#38061=CARTESIAN_POINT('Ctrl Pts',(-3.44906659925855,-8.9590094418331,0.812316594706053));
#38062=CARTESIAN_POINT('Ctrl Pts',(-3.33162770475231,-8.28036687288089,
-3.515570032124));
#38063=CARTESIAN_POINT('Ctrl Pts',(-3.21418881024608,-5.63802501097498,
-7.0097348384512));
#38064=CARTESIAN_POINT('Ctrl Pts',(-3.09674991573984,-1.65861841013657,
-8.84153229039908));
#38065=CARTESIAN_POINT('Ctrl Pts',(-2.97931102123362,2.71413146624106,-8.57654932190911));
#38066=CARTESIAN_POINT('Ctrl Pts',(-2.86187212672738,6.44322197393785,-6.27762700530862));
#38067=CARTESIAN_POINT('Ctrl Pts',(-2.74443323222115,8.6442937759285,-2.4899575744746));
#38068=CARTESIAN_POINT('Ctrl Pts',(-2.62699433771492,8.79536166692642,1.8882083212812));
#38069=CARTESIAN_POINT('Ctrl Pts',(-2.50955544320868,6.86059632465833,5.81858341502198));
#38070=CARTESIAN_POINT('Ctrl Pts',(-2.39211654870245,3.29883642759064,8.36907388675404));
#38071=CARTESIAN_POINT('Ctrl Pts',(-2.27467765419622,-1.04525534929133,
8.93482865489668));
#38072=CARTESIAN_POINT('Ctrl Pts',(-2.15723875968999,-5.14144636706299,
7.38167646863233));
#38073=CARTESIAN_POINT('Ctrl Pts',(-2.03979986518375,-8.01837074545405,
4.07795285537554));
#38074=CARTESIAN_POINT('Ctrl Pts',(-1.92236097067752,-8.99366196424782,
-0.192867001355429));
#38075=CARTESIAN_POINT('Ctrl Pts',(-1.80492207617129,-7.83622611320565,
-4.41793906482233));
#38076=CARTESIAN_POINT('Ctrl Pts',(-1.68748318166506,-4.82016098109842,
-7.59530947601204));
#38077=CARTESIAN_POINT('Ctrl Pts',(-1.57004428715883,-0.661501161554172,
-8.97140598760125));
#38078=CARTESIAN_POINT('Ctrl Pts',(-1.45260539265259,3.6550821937918,-8.22000743827012));
#38079=CARTESIAN_POINT('Ctrl Pts',(-1.3743127963151,5.95323704169039,-6.41925818630909));
#38080=CARTESIAN_POINT('Ctrl Pts',(-1.33516649814636,6.82239825464977,-5.30055113218915));
#38081=CARTESIAN_POINT('Ctrl Pts',(-11.7398335018536,4.84822929958311,-6.80323369131649));
#38082=CARTESIAN_POINT('Ctrl Pts',(-11.7006872036849,5.96379383235061,-6.00824223596748));
#38083=CARTESIAN_POINT('Ctrl Pts',(-11.6223946073474,7.79543266737381,-3.85993105185963));
#38084=CARTESIAN_POINT('Ctrl Pts',(-11.5049557128412,8.69396726206043,0.280394411340654));
#38085=CARTESIAN_POINT('Ctrl Pts',(-11.3875168183349,7.53075696430187,4.35320836797643));
#38086=CARTESIAN_POINT('Ctrl Pts',(-11.2700779238287,4.58160321270218,7.39415014262294));
#38087=CARTESIAN_POINT('Ctrl Pts',(-11.1526390293225,0.545923703805717,
8.68130953564814));
#38088=CARTESIAN_POINT('Ctrl Pts',(-11.0352001348162,-3.61922588497217,
7.90981255230121));
#38089=CARTESIAN_POINT('Ctrl Pts',(-10.91776124031,-6.92606972083871,5.26242918861808));
#38090=CARTESIAN_POINT('Ctrl Pts',(-10.8003223458038,-8.5903884078789,1.36708690845965));
#38091=CARTESIAN_POINT('Ctrl Pts',(-10.6828834512975,-8.21748530084544,
-2.85247835334975));
#38092=CARTESIAN_POINT('Ctrl Pts',(-10.5654445567913,-5.89579554376979,
-6.39556638001792));
#38093=CARTESIAN_POINT('Ctrl Pts',(-10.4480056622851,-2.17591039922154,
-8.42194214584341));
#38094=CARTESIAN_POINT('Ctrl Pts',(-10.3305667677788,2.05999454897933,-8.45104165332889));
#38095=CARTESIAN_POINT('Ctrl Pts',(-10.2131278732726,5.80736925177168,-6.47596719630671));
#38096=CARTESIAN_POINT('Ctrl Pts',(-10.0956889787664,8.1775190775919,-2.9651084812346));
#38097=CARTESIAN_POINT('Ctrl Pts',(-9.97825008426016,8.60836006298699,1.248929123778));
#38098=CARTESIAN_POINT('Ctrl Pts',(-9.8608111897539,6.99771771880634,5.16678177385116));
#38099=CARTESIAN_POINT('Ctrl Pts',(-9.74337229524769,3.72755789195307,7.85932560877514));
#38100=CARTESIAN_POINT('Ctrl Pts',(-9.62593340074144,-0.426596939130836,
8.6880206104666));
#38101=CARTESIAN_POINT('Ctrl Pts',(-9.50849450623522,-4.47958377350399,
7.45634066956625));
#38102=CARTESIAN_POINT('Ctrl Pts',(-9.39105561172899,-7.47023172921315,
4.456380248742));
#38103=CARTESIAN_POINT('Ctrl Pts',(-9.27361671722275,-8.68930491314286,
0.399583688947602));
#38104=CARTESIAN_POINT('Ctrl Pts',(-9.15617782271653,-7.84769859947314,
-3.75197463857764));
#38105=CARTESIAN_POINT('Ctrl Pts',(-9.03873892821029,-5.14500077505786,
-7.01374750226396));
#38106=CARTESIAN_POINT('Ctrl Pts',(-8.92130003370406,-1.22215959988252,
-8.61220139743023));
#38107=CARTESIAN_POINT('Ctrl Pts',(-8.80386113919782,2.99051824872198,-8.16826099016765));
#38108=CARTESIAN_POINT('Ctrl Pts',(-8.6864222446916,6.49399096478861,-5.78720730126397));
#38109=CARTESIAN_POINT('Ctrl Pts',(-8.56898335018535,8.45740562409074,-2.03371018299995));
#38110=CARTESIAN_POINT('Ctrl Pts',(-8.45154445567914,8.41513599135171,2.20208384169883));
#38111=CARTESIAN_POINT('Ctrl Pts',(-8.33410556117289,6.37720636269711,5.91565093682343));
#38112=CARTESIAN_POINT('Ctrl Pts',(-8.21666666666667,2.82691429131802,8.22631403414417));
#38113=CARTESIAN_POINT('Ctrl Pts',(-8.09922777216043,-1.39378403004486,
8.58609649819838));
#38114=CARTESIAN_POINT('Ctrl Pts',(-7.9817888776542,-5.28394473032056,6.90967546891433));
#38115=CARTESIAN_POINT('Ctrl Pts',(-7.86434998314797,-7.92101134753324,
3.59461628425654));
#38116=CARTESIAN_POINT('Ctrl Pts',(-7.74691108864174,-8.67960024439589,
-0.572910635506885));
#38117=CARTESIAN_POINT('Ctrl Pts',(-7.6294721941355,-7.37981111788649,-4.60457108351182));
#38118=CARTESIAN_POINT('Ctrl Pts',(-7.51203329962927,-4.32989058048619,
-7.54425175612604));
#38119=CARTESIAN_POINT('Ctrl Pts',(-7.39459440512304,-0.253131091576217,
-8.69480371539643));
#38120=CARTESIAN_POINT('Ctrl Pts',(-7.2771555106168,3.88365875141243,-7.78337212918486));
#38121=CARTESIAN_POINT('Ctrl Pts',(-7.15971661611057,7.09943407770776,-5.02610413492158));
#38122=CARTESIAN_POINT('Ctrl Pts',(-7.04227772160433,8.63156975788372,-1.07688927637946));
#38123=CARTESIAN_POINT('Ctrl Pts',(-6.92483882709811,8.11671790446888,3.12771121717918));
#38124=CARTESIAN_POINT('Ctrl Pts',(-6.80739993259187,5.67697627663657,6.59057109462445));
#38125=CARTESIAN_POINT('Ctrl Pts',(-6.68996103808565,1.89093264433377,8.49046881705523));
#38126=CARTESIAN_POINT('Ctrl Pts',(-6.5725221435794,-2.34354802299109,8.3768412699972));
#38127=CARTESIAN_POINT('Ctrl Pts',(-6.45508324907318,-6.02225335373217,
6.27663536795438));
#38128=CARTESIAN_POINT('Ctrl Pts',(-6.33764435456695,-8.27277379053132,
2.68791756002525));
#38129=CARTESIAN_POINT('Ctrl Pts',(-6.22020546006071,-8.56139560489652,
-1.53824324970157));
#38130=CARTESIAN_POINT('Ctrl Pts',(-6.10276656555449,-6.81967177357477,
-5.39960775422637));
#38131=CARTESIAN_POINT('Ctrl Pts',(-5.98532767104824,-3.46065427548533,
-7.98044854531116));
#38132=CARTESIAN_POINT('Ctrl Pts',(-5.86788877654203,0.719061700249613,
-8.66871601046131));
#38133=CARTESIAN_POINT('Ctrl Pts',(-5.75044988203577,4.72825129693874,-7.30118666189211));
#38134=CARTESIAN_POINT('Ctrl Pts',(-5.63301098752956,7.61613020136608,-4.20217179023341));
#38135=CARTESIAN_POINT('Ctrl Pts',(-5.51557209302332,8.69783432951228,-0.106606637467579));
#38136=CARTESIAN_POINT('Ctrl Pts',(-5.39813319851709,7.71683619825904,4.01424041233612));
#38137=CARTESIAN_POINT('Ctrl Pts',(-5.28069430401086,4.90578073795857,7.18310534169375));
#38138=CARTESIAN_POINT('Ctrl Pts',(-5.16325540950462,0.931313257039131,
8.64848788032087));
#38139=CARTESIAN_POINT('Ctrl Pts',(-5.04581651499839,-3.26401632434385,
8.06287073152049));
#38140=CARTESIAN_POINT('Ctrl Pts',(-4.92837762049216,-6.68528036344698,
5.56513373252692));
#38141=CARTESIAN_POINT('Ctrl Pts',(-4.81093872598592,-8.52112182630912,
1.74761832789114));
#38142=CARTESIAN_POINT('Ctrl Pts',(-4.6934998314797,-8.33616862030953,-2.48434694287691));
#38143=CARTESIAN_POINT('Ctrl Pts',(-4.57606093697345,-6.17428262892098,
-6.12714623760273));
#38144=CARTESIAN_POINT('Ctrl Pts',(-4.45862204246723,-2.54815781137567,
-8.31688516015095));
#38145=CARTESIAN_POINT('Ctrl Pts',(-4.34118314796099,1.68226580928467,-8.53426439394464));
#38146=CARTESIAN_POINT('Ctrl Pts',(-4.22374425345477,5.51373799506711,-6.72773218256439));
#38147=CARTESIAN_POINT('Ctrl Pts',(-4.10630535894853,8.03762033853134,-3.3257098930997));
#38148=CARTESIAN_POINT('Ctrl Pts',(-3.9888664644423,8.65537099382864,0.865008645433196));
#38149=CARTESIAN_POINT('Ctrl Pts',(-3.87142756993607,7.22048962306834,4.85058930481876));
#38150=CARTESIAN_POINT('Ctrl Pts',(-3.75398867542984,4.07326013198663,7.68584666083514));
#38151=CARTESIAN_POINT('Ctrl Pts',(-3.6365497809236,-0.0399480784137633,
8.69839589516784));
#38152=CARTESIAN_POINT('Ctrl Pts',(-3.51911088641737,-4.1436825546629,7.64810969427759));
#38153=CARTESIAN_POINT('Ctrl Pts',(-3.40167199191113,-7.26473754010695,
4.7840647401377));
#38154=CARTESIAN_POINT('Ctrl Pts',(-3.28423309740491,-8.66295096673114,
0.785472866736996));
#38155=CARTESIAN_POINT('Ctrl Pts',(-3.16679420289867,-8.00673474808114,
-3.39939487798645));
#38156=CARTESIAN_POINT('Ctrl Pts',(-3.04935530839244,-5.45171143488453,
-6.77809188499583));
#38157=CARTESIAN_POINT('Ctrl Pts',(-2.9319164138862,-1.60380788220162,-8.54935595277434));
#38158=CARTESIAN_POINT('Ctrl Pts',(-2.81447751937998,2.62444056588667,-8.29312958333569));
#38159=CARTESIAN_POINT('Ctrl Pts',(-2.69703862487374,6.23029994447327,-6.07017720960104));
#38160=CARTESIAN_POINT('Ctrl Pts',(-2.57959973036751,8.35863536131798,-2.4076747007536));
#38161=CARTESIAN_POINT('Ctrl Pts',(-2.46216083586128,8.50471107882439,1.82581078951133));
#38162=CARTESIAN_POINT('Ctrl Pts',(-2.34472194135504,6.63388178670012,5.62630312507595));
#38163=CARTESIAN_POINT('Ctrl Pts',(-2.22728304684882,3.1898234291443,8.09251035938923));
#38164=CARTESIAN_POINT('Ctrl Pts',(-2.10984415234258,-1.01071395196248,
8.63956925551327));
#38165=CARTESIAN_POINT('Ctrl Pts',(-1.99240525783635,-4.97154267613221,
7.13774237154401));
#38166=CARTESIAN_POINT('Ctrl Pts',(-1.87496636333012,-7.75339651687287,
3.94319325815235));
#38167=CARTESIAN_POINT('Ctrl Pts',(-1.75752746882388,-8.69645836556818,
-0.186493538899628));
#38168=CARTESIAN_POINT('Ctrl Pts',(-1.64008857431765,-7.57727101680884,
-4.27194431940803));
#38169=CARTESIAN_POINT('Ctrl Pts',(-1.52264967981142,-4.66087445293086,
-7.34431568523695));
#38170=CARTESIAN_POINT('Ctrl Pts',(-1.40521078530519,-0.639641264381448,
-8.67493785756361));
#38171=CARTESIAN_POINT('Ctrl Pts',(-1.28777189079895,3.53429673556765,-7.94836994493994));
#38172=CARTESIAN_POINT('Ctrl Pts',(-1.20947929446147,5.75650700228966,-6.20712806162696));
#38173=CARTESIAN_POINT('Ctrl Pts',(-1.17033299629272,6.59694600605871,-5.12538968207745));
#38174=CARTESIAN_POINT('Ctrl Pts',(-11.575,4.68253987355595,-6.57073151046051));
#38175=CARTESIAN_POINT('Ctrl Pts',(-11.5358537018313,5.75997971466614,-5.80290908318214));
#38176=CARTESIAN_POINT('Ctrl Pts',(-11.4575611054938,7.52902184303394,-3.72801696096832));
#38177=CARTESIAN_POINT('Ctrl Pts',(-11.3401222109875,8.39684879745447,0.270811863526706));
#38178=CARTESIAN_POINT('Ctrl Pts',(-11.2226833164813,7.27339149706363,4.20443640376082));
#38179=CARTESIAN_POINT('Ctrl Pts',(-11.1052444219751,4.42502579862193,7.14145324703773));
#38180=CARTESIAN_POINT('Ctrl Pts',(-10.9878055274688,0.527266627263149,
8.38462365194841));
#38181=CARTESIAN_POINT('Ctrl Pts',(-10.8703666329626,-3.49553795222623,
7.63949276732611));
#38182=CARTESIAN_POINT('Ctrl Pts',(-10.7529277384564,-6.68936958853091,
5.08258437974203));
#38183=CARTESIAN_POINT('Ctrl Pts',(-10.6354888439501,-8.29680977603194,
1.32036637789162));
#38184=CARTESIAN_POINT('Ctrl Pts',(-10.5180499494439,-7.93665072418858,
-2.7549942056503));
#38185=CARTESIAN_POINT('Ctrl Pts',(-10.4006110549377,-5.69430528428376,
-6.17699632956363));
#38186=CARTESIAN_POINT('Ctrl Pts',(-10.2831721604314,-2.10154812737837,
-8.1341202063368));
#38187=CARTESIAN_POINT('Ctrl Pts',(-10.1657332659252,1.98959372976295,-8.16222523101317));
#38188=CARTESIAN_POINT('Ctrl Pts',(-10.048294371419,5.60890098251375,-6.25464942822609));
#38189=CARTESIAN_POINT('Ctrl Pts',(-9.93085547691274,7.89805035642209,-2.86377517127619));
#38190=CARTESIAN_POINT('Ctrl Pts',(-9.8134165824065,8.31416724541664,1.20624666449639));
#38191=CARTESIAN_POINT('Ctrl Pts',(-9.69597768790028,6.75856899858617,4.99020573884583));
#38192=CARTESIAN_POINT('Ctrl Pts',(-9.57853879339404,3.60016768628482,7.59073122748412));
#38193=CARTESIAN_POINT('Ctrl Pts',(-9.46109989888781,-0.412017884052814,
8.3911053741381));
#38194=CARTESIAN_POINT('Ctrl Pts',(-9.34366100438158,-4.32649289879303,
7.20151839746173));
#38195=CARTESIAN_POINT('Ctrl Pts',(-9.22622210987535,-7.21493472673645,
4.30408236018371));
#38196=CARTESIAN_POINT('Ctrl Pts',(-9.10878321536912,-8.39234578545526,
0.385927818323404));
#38197=CARTESIAN_POINT('Ctrl Pts',(-8.99134432086288,-7.57950157407817,
-3.62374998460184));
#38198=CARTESIAN_POINT('Ctrl Pts',(-8.87390542635665,-4.96916911103115,
-6.77405096026056));
#38199=CARTESIAN_POINT('Ctrl Pts',(-8.75646653185041,-1.18039199564904,
-8.31787730131265));
#38200=CARTESIAN_POINT('Ctrl Pts',(-8.63902763734419,2.88831655372436,-7.88910866640744));
#38201=CARTESIAN_POINT('Ctrl Pts',(-8.52158874283795,6.27205722999723,-5.5894280716122));
#38202=CARTESIAN_POINT('Ctrl Pts',(-8.40414984833172,8.16837171151259,-1.96420763844087));
#38203=CARTESIAN_POINT('Ctrl Pts',(-8.28671095382549,8.12754665384501,2.12682708603627));
#38204=CARTESIAN_POINT('Ctrl Pts',(-8.16927205931926,6.15926377034014,5.71348211440747));
#38205=CARTESIAN_POINT('Ctrl Pts',(-8.05183316481303,2.73030380171169,7.94517773336033));
#38206=CARTESIAN_POINT('Ctrl Pts',(-7.93439427030679,-1.34615111879544,
8.29266454341796));
#38207=CARTESIAN_POINT('Ctrl Pts',(-7.81695537580056,-5.1033646225271,6.67353561418904));
#38208=CARTESIAN_POINT('Ctrl Pts',(-7.69951648129434,-7.650308840983,3.47176939065404));
#38209=CARTESIAN_POINT('Ctrl Pts',(-7.58207758678809,-8.38297277614415,
-0.553331273951084));
#38210=CARTESIAN_POINT('Ctrl Pts',(-7.46463869228187,-7.12760426199033,
-4.44720873681053));
#38211=CARTESIAN_POINT('Ctrl Pts',(-7.34719979777563,-4.18191550738002,
-7.28642510106571));
#38212=CARTESIAN_POINT('Ctrl Pts',(-7.2297609032694,-0.244480274405397,
-8.39765666479245));
#38213=CARTESIAN_POINT('Ctrl Pts',(-7.11232200876316,3.75093376056635,-7.51737347669715));
#38214=CARTESIAN_POINT('Ctrl Pts',(-6.99488311425694,6.85680917596183,-4.85433579274776));
#38215=CARTESIAN_POINT('Ctrl Pts',(-6.8774442197507,8.33658374329481,-1.04008632109978));
#38216=CARTESIAN_POINT('Ctrl Pts',(-6.76000532524447,7.83932707831064,3.02082091881856));
#38217=CARTESIAN_POINT('Ctrl Pts',(-6.64256643073823,5.48296421930119,6.36533671019601));
#38218=CARTESIAN_POINT('Ctrl Pts',(-6.52512753623201,1.82630955719499,8.20030496174408));
#38219=CARTESIAN_POINT('Ctrl Pts',(-6.40768864172577,-2.26345669421878,
8.09056066399));
#38220=CARTESIAN_POINT('Ctrl Pts',(-6.29024974721954,-5.81644136755901,
6.06212981402202));
#38221=CARTESIAN_POINT('Ctrl Pts',(-6.17281085271331,-7.99004971617214,
2.59605731781944));
#38222=CARTESIAN_POINT('Ctrl Pts',(-6.05537195820707,-8.26880780920608,
-1.48567340917131));
#38223=CARTESIAN_POINT('Ctrl Pts',(-5.93793306370085,-6.58660781722385,
-5.21507483420824));
#38224=CARTESIAN_POINT('Ctrl Pts',(-5.8204941691946,-3.34238556640572,-7.70771475794147));
#38225=CARTESIAN_POINT('Ctrl Pts',(-5.70305527468838,0.694487590192009,
-8.37246051357519));
#38226=CARTESIAN_POINT('Ctrl Pts',(-5.58561638018214,4.56666214859352,-7.0516668160733));
#38227=CARTESIAN_POINT('Ctrl Pts',(-5.46817748567591,7.35584708280132,-4.05856153812523));
#38228=CARTESIAN_POINT('Ctrl Pts',(-5.35073859116968,8.40058370692718,-0.102963329471767));
#38229=CARTESIAN_POINT('Ctrl Pts',(-5.23329969666345,7.45311142753807,3.87705276118435));
#38230=CARTESIAN_POINT('Ctrl Pts',(-5.11586080215721,4.73812447740229,6.93762095396888));
#38231=CARTESIAN_POINT('Ctrl Pts',(-4.99842190765099,0.89948539794352,8.35292368474611));
#38232=CARTESIAN_POINT('Ctrl Pts',(-4.88098301314475,-3.15246776549777,
7.7873201457114));
#38233=CARTESIAN_POINT('Ctrl Pts',(-4.76354411863852,-6.45680926651568,
5.37494392158168));
#38234=CARTESIAN_POINT('Ctrl Pts',(-4.64610522413228,-8.22991039688474,
1.6878930426849));
#38235=CARTESIAN_POINT('Ctrl Pts',(-4.52866632962606,-8.05127801208613,
-2.39944377646666));
#38236=CARTESIAN_POINT('Ctrl Pts',(-4.41122743511982,-5.96327500496155,
-5.91774951138349));
#38237=CARTESIAN_POINT('Ctrl Pts',(-4.29378854061358,-2.46107389287582,
-8.03265356891045));
#38238=CARTESIAN_POINT('Ctrl Pts',(-4.17634964610736,1.62477396243877,-8.24260381404624));
#38239=CARTESIAN_POINT('Ctrl Pts',(-4.05891075160112,5.32530464606164,-6.49781028429742));
#38240=CARTESIAN_POINT('Ctrl Pts',(-3.94147185709489,7.76293269109889,-3.21205294140231));
#38241=CARTESIAN_POINT('Ctrl Pts',(-3.82403296258866,8.35957156616068,0.835446762709816));
#38242=CARTESIAN_POINT('Ctrl Pts',(-3.70659406808243,6.97372761835372,4.68481922503354));
#38243=CARTESIAN_POINT('Ctrl Pts',(-3.58915517357619,3.93405546743286,7.42318096516021));
#38244=CARTESIAN_POINT('Ctrl Pts',(-3.47171627906997,-0.0385828430310631,
8.40112608093868));
#38245=CARTESIAN_POINT('Ctrl Pts',(-3.35427738456373,-4.00207118653311,
7.38673366869508));
#38246=CARTESIAN_POINT('Ctrl Pts',(-3.2368384900575,-7.01646335196947,4.620568153675));
#38247=CARTESIAN_POINT('Ctrl Pts',(-3.11939959555127,-8.36689249162919,
0.758629138767949));
#38248=CARTESIAN_POINT('Ctrl Pts',(-3.00196070104503,-7.73310262328138,
-3.28321972384891));
#38249=CARTESIAN_POINT('Ctrl Pts',(-2.8845218065388,-5.26539785879409,-6.54644893154043));
#38250=CARTESIAN_POINT('Ctrl Pts',(-2.76708291203257,-1.54899735426666,
-8.25717961514961));
#38251=CARTESIAN_POINT('Ctrl Pts',(-2.64964401752634,2.53474966553227,-8.00970984476226));
#38252=CARTESIAN_POINT('Ctrl Pts',(-2.5322051230201,6.01737791500869,-5.86272741389347));
#38253=CARTESIAN_POINT('Ctrl Pts',(-2.41476622851387,8.07297694670747,-2.3253918270326));
#38254=CARTESIAN_POINT('Ctrl Pts',(-2.29732733400764,8.21406049072235,1.76341325774147));
#38255=CARTESIAN_POINT('Ctrl Pts',(-2.17988843950141,6.4071672487419,5.43402283512993));
#38256=CARTESIAN_POINT('Ctrl Pts',(-2.06244954499518,3.08081043069796,7.81594683202442));
#38257=CARTESIAN_POINT('Ctrl Pts',(-1.94501065048894,-0.976172554633629,
8.34430985612986));
#38258=CARTESIAN_POINT('Ctrl Pts',(-1.82757175598271,-4.80163898520143,
6.89380827445569));
#38259=CARTESIAN_POINT('Ctrl Pts',(-1.71013286147648,-7.4884222882917,3.80843366092916));
#38260=CARTESIAN_POINT('Ctrl Pts',(-1.59269396697024,-8.39925476688854,
-0.18012007644382));
#38261=CARTESIAN_POINT('Ctrl Pts',(-1.47525507246401,-7.31831592041203,
-4.12594957399375));
#38262=CARTESIAN_POINT('Ctrl Pts',(-1.35781617795778,-4.50158792476329,
-7.09332189446186));
#38263=CARTESIAN_POINT('Ctrl Pts',(-1.24037728345155,-0.617781367208725,
-8.37846972752598));
#38264=CARTESIAN_POINT('Ctrl Pts',(-1.12293838894532,3.41351127734351,-7.67673245160975));
#38265=CARTESIAN_POINT('Ctrl Pts',(-1.04464579260783,5.55977696288894,-5.99499793694482));
#38266=CARTESIAN_POINT('Ctrl Pts',(-1.00549949443908,6.37149375746765,-4.95022823196575));
#38267=CARTESIAN_POINT('',(-1.5,7.04785050324084,-5.47571258230085));
#38268=CARTESIAN_POINT('Ctrl Pts',(-1.5,-7.40071554151276,-3.21429017473183));
#38269=CARTESIAN_POINT('Ctrl Pts',(-1.5,-7.32607552716124,-3.41408847491103));
#38270=CARTESIAN_POINT('Ctrl Pts',(-1.5,-7.24365422857139,-3.61052987409804));
#38271=CARTESIAN_POINT('Ctrl Pts',(-1.5,-7.1536381226817,-3.80314116313213));
#38272=CARTESIAN_POINT('Ctrl Pts',(-1.5,-7.12529565119459,-3.86378675442481));
#38273=CARTESIAN_POINT('Ctrl Pts',(-1.5,-7.09619986523178,-3.92405263504233));
#38274=CARTESIAN_POINT('Ctrl Pts',(-1.5,-7.06635552234977,-3.98392396459837));
#38275=CARTESIAN_POINT('Ctrl Pts',(-1.5,-6.97243139747263,-4.17234701870998));
#38276=CARTESIAN_POINT('Ctrl Pts',(-1.5,-6.87109710954449,-4.35686339452859));
#38277=CARTESIAN_POINT('Ctrl Pts',(-1.5,-6.76274048915299,-4.53715619452641));
#38278=CARTESIAN_POINT('Ctrl Pts',(-1.5,-6.65334098717867,-4.71918422805175));
#38279=CARTESIAN_POINT('Ctrl Pts',(-1.5,-6.53678300025226,-4.89690755496705));
#38280=CARTESIAN_POINT('Ctrl Pts',(-1.5,-6.41341608194796,-5.06998046755394));
#38281=CARTESIAN_POINT('Ctrl Pts',(-1.5,-6.28977894266464,-5.24343247635658));
#38282=CARTESIAN_POINT('Ctrl Pts',(-1.5,-6.15930261540002,-5.41221423931513));
#38283=CARTESIAN_POINT('Ctrl Pts',(-1.5,-6.0222949455953,-5.5759497740738));
#38284=CARTESIAN_POINT('Ctrl Pts',(-1.5,-5.96511117533728,-5.64428912482739));
#38285=CARTESIAN_POINT('Ctrl Pts',(-1.5,-5.90678913255776,-5.71174902319245));
#38286=CARTESIAN_POINT('Ctrl Pts',(-1.5,-5.84734919270319,-5.77830033033274));
#38287=CARTESIAN_POINT('Ctrl Pts',(-1.5,-5.82312043264619,-5.80542780818899));
#38288=CARTESIAN_POINT('Ctrl Pts',(-1.5,-5.79870591888853,-5.83240430838032));
#38289=CARTESIAN_POINT('Ctrl Pts',(-1.5,-5.77410697966433,-5.85922780040854));
#38290=CARTESIAN_POINT('Ctrl Pts',(-1.5,-5.75257308437455,-5.88270906776637));
#38291=CARTESIAN_POINT('Ctrl Pts',(-1.5,-5.73089516063029,-5.90607586915347));
#38292=CARTESIAN_POINT('Ctrl Pts',(-1.5,-5.70909277099336,-5.92930716662182));
#38293=CARTESIAN_POINT('Ctrl Pts',(-1.5,-5.56150733846096,-6.08656520770133));
#38294=CARTESIAN_POINT('Ctrl Pts',(-1.5,-5.40806704913402,-6.23778842012323));
#38295=CARTESIAN_POINT('Ctrl Pts',(-1.5,-5.24917010701384,-6.38265417970832));
#38296=CARTESIAN_POINT('Ctrl Pts',(-1.5,-5.08916305305425,-6.52853202418754));
#38297=CARTESIAN_POINT('Ctrl Pts',(-1.5,-4.92362244634448,-6.66796384769363));
#38298=CARTESIAN_POINT('Ctrl Pts',(-1.5,-4.75290905048751,-6.80059432958983));
#38299=CARTESIAN_POINT('Ctrl Pts',(-1.5,-4.65550778899749,-6.87626722089323));
#38300=CARTESIAN_POINT('Ctrl Pts',(-1.5,-4.55642181271268,-6.94972553712658));
#38301=CARTESIAN_POINT('Ctrl Pts',(-1.5,-4.45571226131071,-7.02089844525531));
#38302=CARTESIAN_POINT('Ctrl Pts',(-1.5,-4.27985527394039,-7.145179141889));
#38303=CARTESIAN_POINT('Ctrl Pts',(-1.5,-4.09904947818624,-7.26249377733021));
#38304=CARTESIAN_POINT('Ctrl Pts',(-1.5,-3.91376263334626,-7.37270325078949));
#38305=CARTESIAN_POINT('Ctrl Pts',(-1.5,-3.78859158583618,-7.44715556957309));
#38306=CARTESIAN_POINT('Ctrl Pts',(-1.5,-3.66137477543102,-7.51836446454134));
#38307=CARTESIAN_POINT('Ctrl Pts',(-1.5,-3.53224920673504,-7.58627572011563));
#38308=CARTESIAN_POINT('Ctrl Pts',(-1.5,-3.41926433412606,-7.64569806874313));
#38309=CARTESIAN_POINT('Ctrl Pts',(-1.5,-3.30481794856632,-7.70259554193464));
#38310=CARTESIAN_POINT('Ctrl Pts',(-1.5,-3.18899907397327,-7.75692565137345));
#38311=CARTESIAN_POINT('Ctrl Pts',(-1.5,-3.15879244923969,-7.77109544220692));
#38312=CARTESIAN_POINT('Ctrl Pts',(-1.5,-3.12848823906593,-7.78509241552022));
#38313=CARTESIAN_POINT('Ctrl Pts',(-1.5,-3.09811472952744,-7.79890379709708));
#38314=CARTESIAN_POINT('Ctrl Pts',(-1.5,-2.8992287670567,-7.88934082461551));
#38315=CARTESIAN_POINT('Ctrl Pts',(-1.5,-2.69717640931447,-7.97191903960201));
#38316=CARTESIAN_POINT('Ctrl Pts',(-1.5,-2.49247199354083,-8.04655431134645));
#38317=CARTESIAN_POINT('Ctrl Pts',(-1.5,-2.2863262339712,-8.1217150973329));
#38318=CARTESIAN_POINT('Ctrl Pts',(-1.5,-2.07749034379047,-8.18882100549067));
#38319=CARTESIAN_POINT('Ctrl Pts',(-1.5,-1.8664568012609,-8.24774400472739));
#38320=CARTESIAN_POINT('Ctrl Pts',(-1.5,-1.65568015538806,-8.30659527545438));
#38321=CARTESIAN_POINT('Ctrl Pts',(-1.5,-1.44271056686449,-8.35728381421289));
#38322=CARTESIAN_POINT('Ctrl Pts',(-1.5,-1.22801543305964,-8.39963592793665));
#38323=CARTESIAN_POINT('Ctrl Pts',(-1.5,-1.02879612386665,-8.43893518306825));
#38324=CARTESIAN_POINT('Ctrl Pts',(-1.5,-0.82809043936243,-8.4710562447127));
#38325=CARTESIAN_POINT('Ctrl Pts',(-1.5,-0.626261042790105,-8.49582164860091));
#38326=CARTESIAN_POINT('Ctrl Pts',(-1.5,-0.450826239746891,-8.51734831333459));
#38327=CARTESIAN_POINT('Ctrl Pts',(-1.5,-0.274542073599355,-8.53331679425628));
#38328=CARTESIAN_POINT('Ctrl Pts',(-1.5,-0.0976585345107927,-8.54375388314286));
#38329=CARTESIAN_POINT('Ctrl Pts',(-1.5,-0.0616353375598041,-8.54587944728802));
#38330=CARTESIAN_POINT('Ctrl Pts',(-1.5,-0.0255872814160311,-8.54777552216579));
#38331=CARTESIAN_POINT('Ctrl Pts',(-1.5,0.0104835191461953,-8.54944222208194));
#38332=CARTESIAN_POINT('Ctrl Pts',(-1.5,0.0356559460320415,-8.55060534796564));
#38333=CARTESIAN_POINT('Ctrl Pts',(-1.5,0.0608395666875181,-8.55165672685359));
#38334=CARTESIAN_POINT('Ctrl Pts',(-1.5,0.0860189798068464,-8.55259596649835));
#38335=CARTESIAN_POINT('Ctrl Pts',(-1.5,0.304647650635756,-8.56075122866235));
#38336=CARTESIAN_POINT('Ctrl Pts',(-1.5,0.523231328293199,-8.56046971217016));
#38337=CARTESIAN_POINT('Ctrl Pts',(-1.5,0.741283405020929,-8.5519315510966));
#38338=CARTESIAN_POINT('Ctrl Pts',(-1.5,0.962291191374389,-8.54327765471223));
#38339=CARTESIAN_POINT('Ctrl Pts',(-1.5,1.18275348637413,-8.52614180962386));
#38340=CARTESIAN_POINT('Ctrl Pts',(-1.5,1.40217760172751,-8.50066002463597));
#38341=CARTESIAN_POINT('Ctrl Pts',(-1.5,1.62328838446544,-8.47498236648452));
#38342=CARTESIAN_POINT('Ctrl Pts',(-1.5,1.84334564184632,-8.44082997916866));
#38343=CARTESIAN_POINT('Ctrl Pts',(-1.5,2.0618494910781,-8.39828963846045));
#38344=CARTESIAN_POINT('Ctrl Pts',(-1.5,2.27958312201272,-8.35589925094023));
#38345=CARTESIAN_POINT('Ctrl Pts',(-1.5,2.49577496126564,-8.30517986494593));
#38346=CARTESIAN_POINT('Ctrl Pts',(-1.5,2.70992438663794,-8.24616614721805));
#38347=CARTESIAN_POINT('Ctrl Pts',(-1.5,2.85086308604455,-8.20732730088794));
#38348=CARTESIAN_POINT('Ctrl Pts',(-1.5,2.99091699653584,-8.16489481765947));
#38349=CARTESIAN_POINT('Ctrl Pts',(-1.5,3.12993979573812,-8.11886663092679));
#38350=CARTESIAN_POINT('Ctrl Pts',(-1.5,3.17554939098335,-8.10376603606901));
#38351=CARTESIAN_POINT('Ctrl Pts',(-1.5,3.22104797579745,-8.0882783538033));
#38352=CARTESIAN_POINT('Ctrl Pts',(-1.5,3.266430287064,-8.07240329011238));
#38353=CARTESIAN_POINT('Ctrl Pts',(-1.5,3.2928090607661,-8.06317580255341));
#38354=CARTESIAN_POINT('Ctrl Pts',(-1.5,3.31915086873423,-8.05381659336008));
#38355=CARTESIAN_POINT('Ctrl Pts',(-1.5,3.3454470923227,-8.04432832850057));
#38356=CARTESIAN_POINT('Ctrl Pts',(-1.5,3.41180769954115,-8.0203839390939));
#38357=CARTESIAN_POINT('Ctrl Pts',(-1.5,3.47784485409642,-7.99562983843644));
#38358=CARTESIAN_POINT('Ctrl Pts',(-1.5,3.54354309403428,-7.97006958073044));
#38359=CARTESIAN_POINT('Ctrl Pts',(-1.5,3.75098753387345,-7.88936219272456));
#38360=CARTESIAN_POINT('Ctrl Pts',(-1.5,3.95505373021087,-7.80062138510352));
#38361=CARTESIAN_POINT('Ctrl Pts',(-1.5,4.15538780312082,-7.70421697836692));
#38362=CARTESIAN_POINT('Ctrl Pts',(-1.5,4.35776901904387,-7.60682744910566));
#38363=CARTESIAN_POINT('Ctrl Pts',(-1.5,4.55634201706475,-7.50161663005502));
#38364=CARTESIAN_POINT('Ctrl Pts',(-1.5,4.75072757572629,-7.38891433258144));
#38365=CARTESIAN_POINT('Ctrl Pts',(-1.5,4.858921773029,-7.32618470033259));
#38366=CARTESIAN_POINT('Ctrl Pts',(-1.5,4.96581840178216,-7.26113332494834));
#38367=CARTESIAN_POINT('Ctrl Pts',(-1.5,5.07134916269885,-7.1938107550044));
#38368=CARTESIAN_POINT('Ctrl Pts',(-1.5,5.1522016547485,-7.14223150451977));
#38369=CARTESIAN_POINT('Ctrl Pts',(-1.5,5.23225235935691,-7.08931899950226));
#38370=CARTESIAN_POINT('Ctrl Pts',(-1.5,5.31146952438616,-7.03509430816655));
#38371=CARTESIAN_POINT('Ctrl Pts',(-1.5,5.34027476981638,-7.01537692063159));
#38372=CARTESIAN_POINT('Ctrl Pts',(-1.5,5.36897116188161,-6.99548498996351));
#38373=CARTESIAN_POINT('Ctrl Pts',(-1.5,5.39754124998948,-6.97543084519802));
#38374=CARTESIAN_POINT('Ctrl Pts',(-1.5,5.58374239728194,-6.84473104654129));
#38375=CARTESIAN_POINT('Ctrl Pts',(-1.5,5.76473134029108,-6.70704298605941));
#38376=CARTESIAN_POINT('Ctrl Pts',(-1.5,5.94013091598919,-6.56272128494992));
#38377=CARTESIAN_POINT('Ctrl Pts',(-1.5,6.11595427972063,-6.4180508839668));
#38378=CARTESIAN_POINT('Ctrl Pts',(-1.5,6.28616181452858,-6.26671438967896));
#38379=CARTESIAN_POINT('Ctrl Pts',(-1.5,6.45034955006475,-6.10902252251836));
#38380=CARTESIAN_POINT('Ctrl Pts',(-1.5,6.61343122693438,-5.95239295429102));
#38381=CARTESIAN_POINT('Ctrl Pts',(-1.5,6.77057447053939,-5.7894929424118));
#38382=CARTESIAN_POINT('Ctrl Pts',(-1.5,6.92135144632236,-5.62058700655496));
#38383=CARTESIAN_POINT('Ctrl Pts',(-1.5,6.96403155771474,-5.57277516976909));
#38384=CARTESIAN_POINT('Ctrl Pts',(-1.5,7.00620133181954,-5.5244818677487));
#38385=CARTESIAN_POINT('Ctrl Pts',(-1.5,7.04785050324084,-5.47571258230085));
#38386=CARTESIAN_POINT('Ctrl Pts',(-1.5,7.0478505032408,-5.4757125823009));
#38387=CARTESIAN_POINT('Ctrl Pts',(-1.53914629816874,6.14996708109109,-6.63138831099123));
#38388=CARTESIAN_POINT('Ctrl Pts',(-1.57829259633749,4.96291736655354,-7.56151662129575));
#38389=CARTESIAN_POINT('Ctrl Pts',(-1.61743889450623,3.62618772416099,-8.15595230745444));
#38390=CARTESIAN_POINT('Ctrl Pts',(-1.65658519267497,2.28945808176837,-8.75038799361316));
#38391=CARTESIAN_POINT('Ctrl Pts',(-1.69573149084372,0.803048511520739,
-9.00913105562603));
#38392=CARTESIAN_POINT('Ctrl Pts',(-1.73487778901246,-0.656170682026274,
-8.9015741114905));
#38393=CARTESIAN_POINT('Ctrl Pts',(-1.77402408718121,-2.11538987557327,
-8.79401716735496));
#38394=CARTESIAN_POINT('Ctrl Pts',(-1.81317038534995,-3.54741869241963,
-8.32016021707105));
#38395=CARTESIAN_POINT('Ctrl Pts',(-1.8523166835187,-4.7827220508989,-7.53617016583733));
#38396=CARTESIAN_POINT('Ctrl Pts',(-1.89146298168744,-6.01802540937814,
-6.75218011460362));
#38397=CARTESIAN_POINT('Ctrl Pts',(-1.93060927985618,-7.05660330949029,
-5.65805696242012));
#38398=CARTESIAN_POINT('Ctrl Pts',(-1.96975557802493,-7.77517298510053,
-4.38354649525749));
#38399=CARTESIAN_POINT('Ctrl Pts',(-2.00890187619367,-8.49374266071079,
-3.10903602809483));
#38400=CARTESIAN_POINT('Ctrl Pts',(-2.04804817436242,-8.89230411181913,
-1.65413824595303));
#38401=CARTESIAN_POINT('Ctrl Pts',(-2.08719447253116,-8.92366473922459,
-0.191363868813808));
#38402=CARTESIAN_POINT('Ctrl Pts',(-2.0889007065657,-8.92503162632062,-0.127607254679447));
#38403=CARTESIAN_POINT('Ctrl Pts',(-2.09060694060025,-8.92570092469794,
-0.0638356770061805));
#38404=CARTESIAN_POINT('Ctrl Pts',(-2.09231317463479,-8.92567592894044,
-6.35753767513903E-5));
#38405=CARTESIAN_POINT('Origin',(-1.5,8.,0.));
#38406=CARTESIAN_POINT('Origin',(-1.5,0.,0.));
#38407=CARTESIAN_POINT('',(-1.5,-8.,-9.79717439317883E-16));
#38408=CARTESIAN_POINT('Origin',(-1.5,0.,0.));
#38409=CARTESIAN_POINT('Origin',(10.,-4.,2.3094010767585));
#38410=CARTESIAN_POINT('',(5.,-4.,2.3094010767585));
#38411=CARTESIAN_POINT('',(10.,-4.,2.3094010767585));
#38412=CARTESIAN_POINT('',(5.,2.82820063659975E-16,4.61880215351701));
#38413=CARTESIAN_POINT('Origin',(10.,-4.,-2.3094010767585));
#38414=CARTESIAN_POINT('',(5.,-4.,-2.3094010767585));
#38415=CARTESIAN_POINT('',(10.,-4.,-2.3094010767585));
#38416=CARTESIAN_POINT('',(5.,-4.,2.3094010767585));
#38417=CARTESIAN_POINT('Origin',(10.,-1.11022302462516E-15,-4.61880215351701));
#38418=CARTESIAN_POINT('',(5.,-4.,-2.3094010767585));
#38419=CARTESIAN_POINT('Origin',(5.,0.,0.));
#38420=CARTESIAN_POINT('Origin',(2.,-2.3332655251948E-15,-12.7017059221718));
#38421=CARTESIAN_POINT('',(2.,2.75,-11.1139926819003));
#38422=CARTESIAN_POINT('Origin',(2.,-11.,-6.35085296108589));
#38423=CARTESIAN_POINT('',(2.,-8.25,-7.93856620135736));
#38424=CARTESIAN_POINT('Origin',(2.,-11.,6.35085296108588));
#38425=CARTESIAN_POINT('',(2.,-11.,3.17542648054294));
#38426=CARTESIAN_POINT('Origin',(2.,0.,0.));
#38427=CARTESIAN_POINT('',(2.,-12.5,-1.53080849893419E-15));
#38428=CARTESIAN_POINT('Origin',(2.,0.,0.));
#38429=CARTESIAN_POINT('Origin',(0.,12.5,0.));
#38430=CARTESIAN_POINT('',(0.,-12.5,-1.53080849893419E-15));
#38431=CARTESIAN_POINT('Origin',(0.,0.,0.));
#38432=CARTESIAN_POINT('',(0.,-8.,-9.79717439317883E-16));
#38433=CARTESIAN_POINT('Origin',(0.,0.,0.));
#38434=CARTESIAN_POINT('Origin',(1.,0.,0.));
#38435=CARTESIAN_POINT('',(1.,-12.5,-1.53080849893419E-15));
#38436=CARTESIAN_POINT('Origin',(-12.,8.5,0.));
#38437=CARTESIAN_POINT('',(-12.,-8.5,-1.04094977927525E-15));
#38438=CARTESIAN_POINT('Origin',(-12.,0.,0.));
#38439=CARTESIAN_POINT('Origin',(-11.75,0.,0.));
#38440=CARTESIAN_POINT('',(-11.75,-8.75,-1.07156594925393E-15));
#38441=CARTESIAN_POINT('Origin',(-6.5,0.,0.));
#38442=CARTESIAN_POINT('Origin',(-0.75,0.,0.));
#38443=CARTESIAN_POINT('',(-0.75,-8.,-9.79717439317883E-16));
#38489=UNCERTAINTY_MEASURE_WITH_UNIT(LENGTH_MEASURE(0.01),#38508,
'DISTANCE_ACCURACY_VALUE',
'Maximum model space distance between geometric entities at asserted c
onnectivities');
#38490=UNCERTAINTY_MEASURE_WITH_UNIT(LENGTH_MEASURE(0.01),#38508,
'DISTANCE_ACCURACY_VALUE',
'Maximum model space distance between geometric entities at asserted c
onnectivities');
#38506=(
GEOMETRIC_REPRESENTATION_CONTEXT(3)
GLOBAL_UNCERTAINTY_ASSIGNED_CONTEXT((#38489))
GLOBAL_UNIT_ASSIGNED_CONTEXT((#38508,#38510,#38511))
REPRESENTATION_CONTEXT('','3D')
);
#38507=(
GEOMETRIC_REPRESENTATION_CONTEXT(3)
GLOBAL_UNCERTAINTY_ASSIGNED_CONTEXT((#38490))
GLOBAL_UNIT_ASSIGNED_CONTEXT((#38508,#38510,#38511))
REPRESENTATION_CONTEXT('','3D')
);
#38508=(
LENGTH_UNIT()
NAMED_UNIT(*)
SI_UNIT(.MILLI.,.METRE.)
);
#38510=(
NAMED_UNIT(*)
PLANE_ANGLE_UNIT()
SI_UNIT($,.RADIAN.)
);
#38511=(
NAMED_UNIT(*)
SI_UNIT($,.STERADIAN.)
SOLID_ANGLE_UNIT()
);
#38527=SHAPE_DEFINITION_REPRESENTATION(#38543,#38589);
#38543=PRODUCT_DEFINITION_SHAPE('',$,#38606);
#38589=SHAPE_REPRESENTATION('',(#16670),#38506);
#38590=PRODUCT_DEFINITION_CONTEXT('part definition',#38640,'design');
#38606=PRODUCT_DEFINITION('2026-10-26-01-10-59-292',
'15_Drain_Plug_M18x1.5',#38622,#38590);
#38622=PRODUCT_DEFINITION_FORMATION('',$,#38657);
#38640=APPLICATION_CONTEXT(
'Core Data for Automotive Mechanical Design Process');
#38641=PRODUCT_CONTEXT('part definition',#38640,'mechanical');
#38657=PRODUCT('2026-10-26-01-10-59-292','15_Drain_Plug_M18x1.5',$,(#38641));
#38700=COLOUR_RGB('Light Blue',0.38,0.62,0.78);
#38701=FILL_AREA_STYLE_COLOUR('',#38700);
#38702=FILL_AREA_STYLE('',(#38701));
#38703=SURFACE_STYLE_FILL_AREA(#38702);
#38704=SURFACE_SIDE_STYLE('',(#38703));
#38705=SURFACE_STYLE_USAGE(.BOTH.,#38704);
#38706=PRESENTATION_STYLE_ASSIGNMENT((#38705));
ENDSEC;
END-ISO-10303-21;
